ISO-10303-21;
HEADER;
FILE_DESCRIPTION (('STEP AP214'),
    '1' );
FILE_NAME ('Plunger Disc.step',
    '2026-10-06T09:00:30',
    ( '' ),
    ( '' ),
    'SwSTEP 2.0',
    'SolidWorks 2020',
    '' );
FILE_SCHEMA (( 'AUTOMOTIVE_DESIGN' ));
ENDSEC;

DATA;
#9=DIRECTION ( 'NONE',  ( -0.7071067811865475727, 0.7071067811865475727, 0.000000000000000000 ) ) ;
#30=CARTESIAN_POINT ( 'NONE',  ( 1.834951415319072465, -1.057599859260872410, 226.6412452697799438 ) ) ;
#59=DIRECTION ( 'NONE',  ( 0.7071067811865475727, -0.7071067811865475727, 0.000000000000000000 ) ) ;
#81=DIRECTION ( 'NONE',  ( 0.000000000000000000, 0.000000000000000000, 1.000000000000000000 ) ) ;
#125=VERTEX_POINT ( 'NONE', #7091 ) ;
#222=ORIENTED_EDGE ( 'NONE', *, *, #2639, .F. ) ;
#262=DIRECTION ( 'NONE',  ( -0.9595496299847263710, 0.2815395311429191305, 0.000000000000000000 ) ) ;
#313=CARTESIAN_POINT ( 'NONE',  ( -9.502613819449999610, 7.533418146720000763, 230.6412452697800006 ) ) ;
#373=FACE_OUTER_BOUND ( 'NONE', #7279, .T. ) ;
#458=EDGE_CURVE ( 'NONE', #11841, #9298, #9464, .T. ) ;
#461=PLANE ( 'NONE',  #25084 ) ;
#502=CARTESIAN_POINT ( 'NONE',  ( 1.630907767950000142, 5.558498091389999729, 226.6412452697800006 ) ) ;
#541=CARTESIAN_POINT ( 'NONE',  ( 1.776356839399999804E-15, -5.329070518200000398E-15, 224.6412452697800290 ) ) ;
#553=VERTEX_POINT ( 'NONE', #15670 ) ;
#582=DIRECTION ( 'NONE',  ( 0.000000000000000000, 0.000000000000000000, 1.000000000000000000 ) ) ;
#604=DIRECTION ( 'NONE',  ( 0.2815395311429191860, 0.9595496299847263710, 0.000000000000000000 ) ) ;
#648=DIRECTION ( 'NONE',  ( 1.000000000000000000, 0.000000000000000000, 0.000000000000000000 ) ) ;
#671=ORIENTED_EDGE ( 'NONE', *, *, #17096, .T. ) ;
#687=TOROIDAL_SURFACE ( 'NONE', #1239, 12.03781779390000040, 5.000000000000000000 ) ;
#712=FACE_OUTER_BOUND ( 'NONE', #24045, .T. ) ;
#778=ORIENTED_EDGE ( 'NONE', *, *, #1992, .T. ) ;
#861=DIRECTION ( 'NONE',  ( 0.2815395311429196301, 0.9595496299847262600, 0.000000000000000000 ) ) ;
#879=EDGE_CURVE ( 'NONE', #15714, #12853, #23989, .T. ) ;
#908=EDGE_CURVE ( 'NONE', #7204, #15025, #26492, .T. ) ;
#916=ORIENTED_EDGE ( 'NONE', *, *, #7146, .F. ) ;
#1001=EDGE_CURVE ( 'NONE', #23549, #20463, #10068, .T. ) ;
#1073=CARTESIAN_POINT ( 'NONE',  ( 0.000000000000000000, -1.776356839399999804E-15, 227.6412452697800006 ) ) ;
#1085=SHAPE_DEFINITION_REPRESENTATION ( #1867, #27424 ) ;
#1165=AXIS2_PLACEMENT_3D ( 'NONE', #23386, #2435, #6999 ) ;
#1173=CARTESIAN_POINT ( 'NONE',  ( 3.389121577670000107, 11.55088360999999963, 224.6412452697800290 ) ) ;
#1193=AXIS2_PLACEMENT_3D ( 'NONE', #12409, #5331, #2662 ) ;
#1230=EDGE_CURVE ( 'NONE', #7767, #14785, #9674, .T. ) ;
#1239=AXIS2_PLACEMENT_3D ( 'NONE', #10395, #13052, #5970 ) ;
#1249=COLOUR_RGB ( '', 0.40784314, 0.44705882, 0.49803922) ;
#1263=CARTESIAN_POINT ( 'NONE',  ( 0.1656472034149999717, -5.899424820049999241, 226.6412452697800006 ) ) ;
#1306=CARTESIAN_POINT ( 'NONE',  ( 1.776356839399999804E-15, -5.329070518200000398E-15, 228.3912452697800006 ) ) ;
#1322=ORIENTED_EDGE ( 'NONE', *, *, #23592, .F. ) ;
#1410=DIRECTION ( 'NONE',  ( 0.000000000000000000, 0.000000000000000000, 1.000000000000000000 ) ) ;
#1419=CARTESIAN_POINT ( 'NONE',  ( 5.799375405969999342, 1.094484689620000006, 226.6412452697800006 ) ) ;
#1445=CIRCLE ( 'NONE', #16504, 2.100000000000000089 ) ;
#1488=CARTESIAN_POINT ( 'NONE',  ( 1.484924240490000047, -1.484924240490000047, 226.6412452697800006 ) ) ;
#1552=EDGE_CURVE ( 'NONE', #23036, #12853, #28911, .T. ) ;
#1605=CARTESIAN_POINT ( 'NONE',  ( 5.160560622299999345, 6.288231966779999738, 227.7662452697800006 ) ) ;
#1662=ORIENTED_EDGE ( 'NONE', *, *, #19198, .F. ) ;
#1678=CARTESIAN_POINT ( 'NONE',  ( -1.630907768819999992, -5.558498092260000689, 226.6412452697800006 ) ) ;
#1696=FACE_BOUND ( 'NONE', #18455, .T. ) ;
#1726=EDGE_CURVE ( 'NONE', #125, #7204, #1445, .T. ) ;
#1749=DIRECTION ( 'NONE',  ( 1.000000000000000000, 0.000000000000000000, 0.000000000000000000 ) ) ;
#1835=CARTESIAN_POINT ( 'NONE',  ( 1.630907767950000142, 5.558498091389999729, 226.6412452697800006 ) ) ;
#1867=PRODUCT_DEFINITION_SHAPE ( 'NONE', 'NONE',  #15813 ) ;
#1907=EDGE_LOOP ( 'NONE', ( #7559, #15440 ) ) ;
#1921=AXIS2_PLACEMENT_3D ( 'NONE', #21953, #5105, #17369 ) ;
#1936=TOROIDAL_SURFACE ( 'NONE', #28572, 12.03781779390000040, 6.000000000000000000 ) ;
#1959=VERTEX_POINT ( 'NONE', #25081 ) ;
#1992=EDGE_CURVE ( 'NONE', #5428, #16559, #22508, .T. ) ;
#1996=CARTESIAN_POINT ( 'NONE',  ( 0.7577809307819999285, 5.814680484680000205, 226.6412452697800006 ) ) ;
#2009=CARTESIAN_POINT ( 'NONE',  ( -3.389121577140000063, -11.55088360979999962, 230.6412452697800006 ) ) ;
#2053=FACE_OUTER_BOUND ( 'NONE', #14291, .T. ) ;
#2132=ADVANCED_FACE ( 'NONE', ( #23043 ), #25557, .F. ) ;
#2142=CARTESIAN_POINT ( 'NONE',  ( -3.389121647030000073, -11.55088358959999972, 229.6412452697800006 ) ) ;
#2143=EDGE_CURVE ( 'NONE', #28317, #14785, #23667, .T. ) ;
#2146=DIRECTION ( 'NONE',  ( 0.9595496299847263710, -0.2815395311429191305, 0.000000000000000000 ) ) ;
#2155=ORIENTED_EDGE ( 'NONE', *, *, #21760, .T. ) ;
#2204=DIRECTION ( 'NONE',  ( 0.000000000000000000, 0.000000000000000000, 1.000000000000000000 ) ) ;
#2216=DIRECTION ( 'NONE',  ( 0.000000000000000000, 0.000000000000000000, 1.000000000000000000 ) ) ;
#2261=SURFACE_SIDE_STYLE ('',( #21449 ) ) ;
#2262=CIRCLE ( 'NONE', #9195, 5.792819795729999832 ) ;
#2269=DIRECTION ( 'NONE',  ( 1.000000000000000000, 0.000000000000000000, 0.000000000000000000 ) ) ;
#2307=CARTESIAN_POINT ( 'NONE',  ( -4.054393030549999999, -4.288653550910000334, 226.6412452697800006 ) ) ;
#2386=CARTESIAN_POINT ( 'NONE',  ( 1.776356839399999804E-15, -5.329070518200000398E-15, 224.6412452697800290 ) ) ;
#2415=CYLINDRICAL_SURFACE ( 'NONE', #4772, 2.100000000000000977 ) ;
#2427=ORIENTED_EDGE ( 'NONE', *, *, #17591, .T. ) ;
#2435=DIRECTION ( 'NONE',  ( 0.000000000000000000, 0.000000000000000000, 1.000000000000000000 ) ) ;
#2560=( NAMED_UNIT ( * ) SI_UNIT ( $, .STERADIAN. ) SOLID_ANGLE_UNIT ( ) );
#2593=AXIS2_PLACEMENT_3D ( 'NONE', #3415, #27187, #12869 ) ;
#2600=CARTESIAN_POINT ( 'NONE',  ( -1.992768273746703400, -0.6766242680978976631, 226.6412452697800006 ) ) ;
#2627=CARTESIAN_POINT ( 'NONE',  ( 0.000000000000000000, 0.000000000000000000, 0.000000000000000000 ) ) ;
#2639=EDGE_CURVE ( 'NONE', #17407, #15025, #4686, .T. ) ;
#2644=CARTESIAN_POINT ( 'NONE',  ( 3.389121577140000063, 11.55088360979999962, 230.6412452697800006 ) ) ;
#2645=ORIENTED_EDGE ( 'NONE', *, *, #879, .T. ) ;
#2646=DIRECTION ( 'NONE',  ( 1.000000000000000000, 0.000000000000000000, 0.000000000000000000 ) ) ;
#2662=DIRECTION ( 'NONE',  ( 0.2815395311429191860, 0.9595496299847263710, 0.000000000000000000 ) ) ;
#2675=AXIS2_PLACEMENT_3D ( 'NONE', #9937, #3151, #14511 ) ;
#2697=CYLINDRICAL_SURFACE ( 'NONE', #5182, 2.100000000000000977 ) ;
#2711=FILL_AREA_STYLE ('',( #5071 ) ) ;
#2713=VERTEX_POINT ( 'NONE', #29065 ) ;
#2720=DIRECTION ( 'NONE',  ( 0.2815395311429191860, 0.9595496299847262600, 0.000000000000000000 ) ) ;
#2810=CARTESIAN_POINT ( 'NONE',  ( -11.93900533819999943, 2.124654348349999999, 230.6412452697800006 ) ) ;
#2829=EDGE_LOOP ( 'NONE', ( #19362, #23310, #17776, #25400 ) ) ;
#2850=DIRECTION ( 'NONE',  ( 0.000000000000000000, 0.000000000000000000, 1.000000000000000000 ) ) ;
#2901=DIRECTION ( 'NONE',  ( 1.000000000000000000, 0.000000000000000000, 0.000000000000000000 ) ) ;
#2948=DIRECTION ( 'NONE',  ( -0.9595496299847263710, 0.2815395311429191305, 0.000000000000000000 ) ) ;
#2962=FACE_OUTER_BOUND ( 'NONE', #28524, .T. ) ;
#3048=EDGE_LOOP ( 'NONE', ( #26864, #12144, #12878, #9117 ) ) ;
#3058=DIRECTION ( 'NONE',  ( 0.000000000000000000, 0.000000000000000000, 1.000000000000000000 ) ) ;
#3097=UNCERTAINTY_MEASURE_WITH_UNIT (LENGTH_MEASURE( 1.000000000000000082E-05 ), #5843, 'distance_accuracy_value', 'NONE');
#3145=DIRECTION ( 'NONE',  ( 0.000000000000000000, 0.000000000000000000, 1.000000000000000000 ) ) ;
#3151=DIRECTION ( 'NONE',  ( 0.000000000000000000, 0.000000000000000000, 1.000000000000000000 ) ) ;
#3185=AXIS2_PLACEMENT_3D ( 'NONE', #21699, #12091, #24065 ) ;
#3243=ORIENTED_EDGE ( 'NONE', *, *, #10470, .T. ) ;
#3311=CARTESIAN_POINT ( 'NONE',  ( 2.100000000000000089, -1.998401444330000344E-15, 227.6412452697800006 ) ) ;
#3313=CARTESIAN_POINT ( 'NONE',  ( 1.386473476218618162, 1.583312407046600701, 226.6412452697799722 ) ) ;
#3363=CARTESIAN_POINT ( 'NONE',  ( 0.000000000000000000, 0.000000000000000000, 227.6412452697800006 ) ) ;
#3383=( GEOMETRIC_REPRESENTATION_CONTEXT ( 3 ) GLOBAL_UNCERTAINTY_ASSIGNED_CONTEXT ( ( #3097 ) ) GLOBAL_UNIT_ASSIGNED_CONTEXT ( ( #5843, #20791, #6619 ) ) REPRESENTATION_CONTEXT ( 'NONE', 'WORKASPACE' ) );
#3408=EDGE_LOOP ( 'NONE', ( #7245, #6022, #18456, #25716 ) ) ;
#3415=CARTESIAN_POINT ( 'NONE',  ( 1.776356839399999804E-15, -5.329070518200000398E-15, 224.6412452697800290 ) ) ;
#3426=AXIS2_PLACEMENT_3D ( 'NONE', #4392, #11934, #2646 ) ;
#3431=ORIENTED_EDGE ( 'NONE', *, *, #12893, .T. ) ;
#3478=PRESENTATION_STYLE_ASSIGNMENT (( #17793 ) ) ;
#3520=DIRECTION ( 'NONE',  ( 0.7730139489027949562, -0.6343890248118320141, 0.000000000000000000 ) ) ;
#3588=AXIS2_PLACEMENT_3D ( 'NONE', #22123, #15345, #17083 ) ;
#3632=FILL_AREA_STYLE ('',( #20473 ) ) ;
#3657=ORIENTED_EDGE ( 'NONE', *, *, #18560, .F. ) ;
#3667=DIRECTION ( 'NONE',  ( 0.000000000000000000, 0.000000000000000000, 1.000000000000000000 ) ) ;
#3668=CARTESIAN_POINT ( 'NONE',  ( 0.5496705564632800023, -2.045342621171242659, 226.6412452697799438 ) ) ;
#3762=CARTESIAN_POINT ( 'NONE',  ( -8.881784197000000993E-16, -8.881784197000000993E-16, 227.6412452697800006 ) ) ;
#3782=DIRECTION ( 'NONE',  ( -0.7071067811865475727, -0.7071067811865475727, 0.000000000000000000 ) ) ;
#3797=ORIENTED_EDGE ( 'NONE', *, *, #23034, .T. ) ;
#3844=CARTESIAN_POINT ( 'NONE',  ( 0.000000000000000000, 0.000000000000000000, 229.6412452697800006 ) ) ;
#3886=CARTESIAN_POINT ( 'NONE',  ( 0.000000000000000000, -1.776356839399999804E-15, 227.6412452697800006 ) ) ;
#3929=EDGE_CURVE ( 'NONE', #5428, #14489, #25321, .T. ) ;
#3936=AXIS2_PLACEMENT_3D ( 'NONE', #19516, #16526, #24231 ) ;
#3992=ORIENTED_EDGE ( 'NONE', *, *, #908, .F. ) ;
#4012=CARTESIAN_POINT ( 'NONE',  ( 18.00000000000000000, 0.000000000000000000, 229.6412452697800006 ) ) ;
#4041=DIRECTION ( 'NONE',  ( 0.000000000000000000, 0.000000000000000000, 1.000000000000000000 ) ) ;
#4085=CARTESIAN_POINT ( 'NONE',  ( 1.630907767950000142, 5.558498091389999729, 226.6412452697800006 ) ) ;
#4101=CARTESIAN_POINT ( 'NONE',  ( 0.000000000000000000, 0.000000000000000000, 227.6412452697800006 ) ) ;
#4122=PRODUCT ( 'Plunger Disc', 'Plunger Disc', '', ( #18536 ) ) ;
#4150=ADVANCED_FACE ( 'NONE', ( #19170 ), #14611, .F. ) ;
#4188=DIRECTION ( 'NONE',  ( 0.2815395311429191305, 0.9595496299847263710, 0.000000000000000000 ) ) ;
#4250=AXIS2_PLACEMENT_3D ( 'NONE', #19682, #3145, #13482 ) ;
#4255=DIRECTION ( 'NONE',  ( 0.000000000000000000, 0.000000000000000000, 1.000000000000000000 ) ) ;
#4257=DIRECTION ( 'NONE',  ( 0.000000000000000000, 0.000000000000000000, 1.000000000000000000 ) ) ;
#4262=ORIENTED_EDGE ( 'NONE', *, *, #7146, .T. ) ;
#4364=CARTESIAN_POINT ( 'NONE',  ( 0.000000000000000000, 0.000000000000000000, 230.6412452697800006 ) ) ;
#4384=AXIS2_PLACEMENT_3D ( 'NONE', #29143, #9490, #2720 ) ;
#4392=CARTESIAN_POINT ( 'NONE',  ( -8.881784197000000993E-16, -8.881784197000000993E-16, 227.6412452697800006 ) ) ;
#4402=VECTOR ( 'NONE', #1410, 1000.000000000000000 ) ;
#4406=AXIS2_PLACEMENT_3D ( 'NONE', #24968, #2948, #604 ) ;
#4407=DIRECTION ( 'NONE',  ( 1.000000000000000000, 0.000000000000000000, 0.000000000000000000 ) ) ;
#4553=CARTESIAN_POINT ( 'NONE',  ( -4.595673019280000382, -11.13819881049999871, 230.6412452697800006 ) ) ;
#4582=DIRECTION ( 'NONE',  ( 0.000000000000000000, 0.000000000000000000, 1.000000000000000000 ) ) ;
#4635=CARTESIAN_POINT ( 'NONE',  ( -18.00000000000000000, 2.204291436879999808E-15, 229.6412452697800006 ) ) ;
#4643=CYLINDRICAL_SURFACE ( 'NONE', #1921, 2.100000000000000977 ) ;
#4650=CARTESIAN_POINT ( 'NONE',  ( 3.389121577680000108, 11.55088360999999963, 224.6412452697800290 ) ) ;
#4686=LINE ( 'NONE', #4996, #8548 ) ;
#4705=CARTESIAN_POINT ( 'NONE',  ( -7.428896285829999613, -9.584552481639999399, 230.6412452697800006 ) ) ;
#4739=AXIS2_PLACEMENT_3D ( 'NONE', #23387, #7000, #20862 ) ;
#4772=AXIS2_PLACEMENT_3D ( 'NONE', #29294, #9958, #19558 ) ;
#4773=( LENGTH_UNIT ( ) NAMED_UNIT ( * ) SI_UNIT ( .MILLI., .METRE. ) );
#4792=VERTEX_POINT ( 'NONE', #11862 ) ;
#4846=EDGE_LOOP ( 'NONE', ( #14823, #29844, #10226, #4995 ) ) ;
#4965=UNCERTAINTY_MEASURE_WITH_UNIT (LENGTH_MEASURE( 1.000000000000000082E-05 ), #4773, 'distance_accuracy_value', 'NONE');
#4995=ORIENTED_EDGE ( 'NONE', *, *, #19018, .F. ) ;
#4996=CARTESIAN_POINT ( 'NONE',  ( 2.220446049249999755E-16, 2.100000000000000089, 227.6412452697800006 ) ) ;
#5000=CARTESIAN_POINT ( 'NONE',  ( 1.992768273684766056, 0.6766242665914681265, 226.6412452697800006 ) ) ;
#5017=LINE ( 'NONE', #26268, #7281 ) ;
#5036=VERTEX_POINT ( 'NONE', #25207 ) ;
#5071=FILL_AREA_STYLE_COLOUR ( '', #1249 ) ;
#5105=DIRECTION ( 'NONE',  ( 0.000000000000000000, 0.000000000000000000, 1.000000000000000000 ) ) ;
#5136=AXIS2_PLACEMENT_3D ( 'NONE', #26345, #14391, #11403 ) ;
#5142=ORIENTED_EDGE ( 'NONE', *, *, #1726, .T. ) ;
#5159=CARTESIAN_POINT ( 'NONE',  ( 2.247467472219999429, 11.88585404949999891, 230.6412452697800006 ) ) ;
#5175=TOROIDAL_SURFACE ( 'NONE', #1165, 5.792819795519999815, 3.000000000000000000 ) ;
#5182=AXIS2_PLACEMENT_3D ( 'NONE', #12295, #2850, #10699 ) ;
#5221=ORIENTED_EDGE ( 'NONE', *, *, #26186, .F. ) ;
#5236=ADVANCED_FACE ( 'NONE', ( #11829 ), #24902, .F. ) ;
#5263=FACE_BOUND ( 'NONE', #13903, .T. ) ;
#5310=CARTESIAN_POINT ( 'NONE',  ( 1.484924240490000047, 1.484924240490000047, 226.6412452697800006 ) ) ;
#5324=CARTESIAN_POINT ( 'NONE',  ( 3.389121577690000109, 11.55088360999999963, 229.6412452697800006 ) ) ;
#5331=DIRECTION ( 'NONE',  ( 0.9595496299847263710, -0.2815395311429191305, 0.000000000000000000 ) ) ;
#5388=CIRCLE ( 'NONE', #14969, 2.100000000000000089 ) ;
#5428=VERTEX_POINT ( 'NONE', #29579 ) ;
#5461=CARTESIAN_POINT ( 'NONE',  ( -8.881784197000000993E-16, -8.881784197000000993E-16, 227.6412452697800006 ) ) ;
#5479=EDGE_CURVE ( 'NONE', #14785, #7767, #23866, .T. ) ;
#5480=CARTESIAN_POINT ( 'NONE',  ( -1.822228222620360105, 1.053429627095256338, 226.6412452697799722 ) ) ;
#5533=VERTEX_POINT ( 'NONE', #502 ) ;
#5564=DIRECTION ( 'NONE',  ( 0.000000000000000000, 0.000000000000000000, 1.000000000000000000 ) ) ;
#5646=AXIS2_PLACEMENT_3D ( 'NONE', #24078, #14633, #9431 ) ;
#5825=ORIENTED_EDGE ( 'NONE', *, *, #18275, .T. ) ;
#5843=( LENGTH_UNIT ( ) NAMED_UNIT ( * ) SI_UNIT ( .MILLI., .METRE. ) );
#5846=CARTESIAN_POINT ( 'NONE',  ( 2.100000000115434418, -0.2748893566605633554, 226.6412452697800575 ) ) ;
#5874=CIRCLE ( 'NONE', #4384, 2.999999999999998668 ) ;
#5879=DIRECTION ( 'NONE',  ( 1.000000000000000000, 0.000000000000000000, 0.000000000000000000 ) ) ;
#5970=DIRECTION ( 'NONE',  ( 0.2815395311429195746, 0.9595496299847261490, 0.000000000000000000 ) ) ;
#6022=ORIENTED_EDGE ( 'NONE', *, *, #6408, .F. ) ;
#6123=CARTESIAN_POINT ( 'NONE',  ( 5.899424784619999862, 0.1656472027260000035, 226.6412452697800006 ) ) ;
#6129=AXIS2_PLACEMENT_3D ( 'NONE', #4364, #18038, #9077 ) ;
#6226=ORIENTED_EDGE ( 'NONE', *, *, #30860, .T. ) ;
#6284=CARTESIAN_POINT ( 'NONE',  ( 2.070461221339999991, 7.056594471000000368, 228.3912452697800006 ) ) ;
#6345=ORIENTED_EDGE ( 'NONE', *, *, #16479, .F. ) ;
#6403=MECHANICAL_DESIGN_GEOMETRIC_PRESENTATION_REPRESENTATION('',(#25502),#3383);
#6407=AXIS2_PLACEMENT_3D ( 'NONE', #541, #28421, #26219 ) ;
#6408=EDGE_CURVE ( 'NONE', #16559, #16947, #5017, .T. ) ;
#6543=ADVANCED_FACE ( 'NONE', ( #373 ), #2415, .F. ) ;
#6619=( NAMED_UNIT ( * ) SI_UNIT ( $, .STERADIAN. ) SOLID_ANGLE_UNIT ( ) );
#6651=ORIENTED_EDGE ( 'NONE', *, *, #18385, .T. ) ;
#6664=DIRECTION ( 'NONE',  ( 0.6343890248118319031, 0.7730139489027950672, 0.000000000000000000 ) ) ;
#6686=CARTESIAN_POINT ( 'NONE',  ( 4.665340848529999640, 5.684798146329999469, 228.3912452697800006 ) ) ;
#6853=CARTESIAN_POINT ( 'NONE',  ( -5.240471012809999607, -2.862882362280000148, 226.6412452697800006 ) ) ;
#6866=CARTESIAN_POINT ( 'NONE',  ( 11.08631338020000001, 4.914038141549999850, 230.6412452697800006 ) ) ;
#6940=CARTESIAN_POINT ( 'NONE',  ( 1.484924240490000047, -1.484924240490000047, 226.6412452697800006 ) ) ;
#6954=APPLICATION_CONTEXT ( 'automotive_design' ) ;
#6999=DIRECTION ( 'NONE',  ( 0.2815395311429195746, 0.9595496299847261490, 0.000000000000000000 ) ) ;
#7000=DIRECTION ( 'NONE',  ( 0.000000000000000000, 0.000000000000000000, 1.000000000000000000 ) ) ;
#7058=ORIENTED_EDGE ( 'NONE', *, *, #12156, .T. ) ;
#7091=CARTESIAN_POINT ( 'NONE',  ( 2.100000000000000089, -1.998401444330000344E-15, 227.6412452697800006 ) ) ;
#7146=EDGE_CURVE ( 'NONE', #19698, #5036, #29129, .T. ) ;
#7167=EDGE_CURVE ( 'NONE', #5533, #21014, #14219, .T. ) ;
#7183=CARTESIAN_POINT ( 'NONE',  ( 11.51831195910000005, 3.792349640119999865, 230.6412452697800006 ) ) ;
#7204=VERTEX_POINT ( 'NONE', #23863 ) ;
#7221=CARTESIAN_POINT ( 'NONE',  ( -11.08631337909999992, -4.914038143670000025, 230.6412452697800006 ) ) ;
#7245=ORIENTED_EDGE ( 'NONE', *, *, #15837, .T. ) ;
#7254=CARTESIAN_POINT ( 'NONE',  ( -3.389121647030000073, -11.55088358959999972, 224.6412452697800290 ) ) ;
#7274=ORIENTED_EDGE ( 'NONE', *, *, #21760, .F. ) ;
#7279=EDGE_LOOP ( 'NONE', ( #25249, #222, #29206, #18058 ) ) ;
#7281=VECTOR ( 'NONE', #19344, 1000.000000000000000 ) ;
#7312=LINE ( 'NONE', #4635, #29858 ) ;
#7325=CARTESIAN_POINT ( 'NONE',  ( -1.484924240490000047, -1.484924240490000047, 226.6412452697800006 ) ) ;
#7361=CARTESIAN_POINT ( 'NONE',  ( 2.100000000000000089, -1.998401444330000344E-15, 226.6412452697800006 ) ) ;
#7364=DIRECTION ( 'NONE',  ( 0.000000000000000000, 0.000000000000000000, 1.000000000000000000 ) ) ;
#7375=CARTESIAN_POINT ( 'NONE',  ( -11.51831195970000010, -3.792349639629999825, 230.6412452697800006 ) ) ;
#7395=AXIS2_PLACEMENT_3D ( 'NONE', #1173, #20364, #24779 ) ;
#7430=VECTOR ( 'NONE', #13987, 1000.000000000000000 ) ;
#7453=DIRECTION ( 'NONE',  ( 1.000000000000000000, 0.000000000000000000, 0.000000000000000000 ) ) ;
#7473=CARTESIAN_POINT ( 'NONE',  ( -1.834980887776583636, -1.057731052603296362, 226.6412452697800006 ) ) ;
#7485=EDGE_CURVE ( 'NONE', #15025, #16515, #21600, .T. ) ;
#7518=DIRECTION ( 'NONE',  ( 0.000000000000000000, 0.000000000000000000, 1.000000000000000000 ) ) ;
#7519=ORIENTED_EDGE ( 'NONE', *, *, #1726, .F. ) ;
#7559=ORIENTED_EDGE ( 'NONE', *, *, #1230, .F. ) ;
#7578=ADVANCED_FACE ( 'NONE', ( #8080 ), #23607, .T. ) ;
#7660=DIRECTION ( 'NONE',  ( -0.7071067811865475727, -0.7071067811865475727, 0.000000000000000000 ) ) ;
#7712=CIRCLE ( 'NONE', #10724, 2.100000000000000089 ) ;
#7724=ORIENTED_EDGE ( 'NONE', *, *, #9895, .T. ) ;
#7767=VERTEX_POINT ( 'NONE', #8046 ) ;
#7770=FACE_OUTER_BOUND ( 'NONE', #2829, .T. ) ;
#7780=DIRECTION ( 'NONE',  ( 0.2815395311429191305, 0.9595496299847263710, 0.000000000000000000 ) ) ;
#7834=CARTESIAN_POINT ( 'NONE',  ( -1.887507898140760254, 0.9307262473892381482, 226.6412452697800290 ) ) ;
#7874=CARTESIAN_POINT ( 'NONE',  ( 1.484924240490000047, 1.484924240490000047, 226.6412452697800006 ) ) ;
#7900=CARTESIAN_POINT ( 'NONE',  ( -4.884981308350000102E-15, -2.100000000000000089, 226.6412452697800006 ) ) ;
#7959=ORIENTED_EDGE ( 'NONE', *, *, #11817, .F. ) ;
#7966=ORIENTED_EDGE ( 'NONE', *, *, #17591, .F. ) ;
#8028=CARTESIAN_POINT ( 'NONE',  ( 7.105427357599999217E-15, 8.881784197000000993E-16, 227.7662452697800006 ) ) ;
#8046=CARTESIAN_POINT ( 'NONE',  ( -18.00000000000000000, 3.980648276280000204E-15, 229.6412452697800006 ) ) ;
#8080=FACE_OUTER_BOUND ( 'NONE', #10097, .T. ) ;
#8084=UNCERTAINTY_MEASURE_WITH_UNIT (LENGTH_MEASURE( 1.000000000000000082E-05 ), #18925, 'distance_accuracy_value', 'NONE');
#8131=DIRECTION ( 'NONE',  ( 0.000000000000000000, 0.000000000000000000, -1.000000000000000000 ) ) ;
#8136=CARTESIAN_POINT ( 'NONE',  ( -2.045530030620520634, 0.5496038860227483447, 226.6412452697800575 ) ) ;
#8185=ORIENTED_EDGE ( 'NONE', *, *, #18082, .T. ) ;
#8190=SURFACE_STYLE_FILL_AREA ( #3632 ) ;
#8387=CARTESIAN_POINT ( 'NONE',  ( 7.636659491129999644, 9.305401069029999306, 224.6412452697800290 ) ) ;
#8448=EDGE_CURVE ( 'NONE', #10023, #23549, #11926, .T. ) ;
#8495=ADVANCED_FACE ( 'NONE', ( #8588 ), #25000, .T. ) ;
#8548=VECTOR ( 'NONE', #17103, 1000.000000000000000 ) ;
#8561=FACE_OUTER_BOUND ( 'NONE', #4846, .T. ) ;
#8578=ORIENTED_EDGE ( 'NONE', *, *, #18385, .F. ) ;
#8588=FACE_OUTER_BOUND ( 'NONE', #19396, .T. ) ;
#8689=ORIENTED_EDGE ( 'NONE', *, *, #1992, .F. ) ;
#8691=EDGE_LOOP ( 'NONE', ( #1662, #4262, #11034, #8578 ) ) ;
#8859=CARTESIAN_POINT ( 'NONE',  ( 1.057599857924298670, -1.834951416016458614, 226.6412452697800290 ) ) ;
#8881=CYLINDRICAL_SURFACE ( 'NONE', #4739, 18.00000000000000000 ) ;
#8918=CARTESIAN_POINT ( 'NONE',  ( 8.136960026420000602, 8.894733314490000708, 230.6412452697800006 ) ) ;
#8937=TOROIDAL_SURFACE ( 'NONE', #21503, 5.792819795519999815, 2.000000000000000000 ) ;
#9007=AXIS2_PLACEMENT_3D ( 'NONE', #3844, #29651, #30118 ) ;
#9074=CARTESIAN_POINT ( 'NONE',  ( -1.484924240490000047, -1.484924240490000047, 227.6412452697800006 ) ) ;
#9075=CARTESIAN_POINT ( 'NONE',  ( -1.064429458170000231, -12.07977735470000091, 230.6412452697800006 ) ) ;
#9077=DIRECTION ( 'NONE',  ( 1.000000000000000000, 0.000000000000000000, 0.000000000000000000 ) ) ;
#9089=ORIENTED_EDGE ( 'NONE', *, *, #15359, .F. ) ;
#9117=ORIENTED_EDGE ( 'NONE', *, *, #7167, .T. ) ;
#9160=CIRCLE ( 'NONE', #5136, 7.354069295110000404 ) ;
#9195=AXIS2_PLACEMENT_3D ( 'NONE', #27303, #12517, #19921 ) ;
#9196=ADVANCED_FACE ( 'NONE', ( #7770 ), #4643, .F. ) ;
#9201=CIRCLE ( 'NONE', #2675, 5.792819795729999832 ) ;
#9245=ADVANCED_FACE ( 'NONE', ( #5263, #14252 ), #9672, .F. ) ;
#9298=VERTEX_POINT ( 'NONE', #22718 ) ;
#9323=ORIENTED_EDGE ( 'NONE', *, *, #12491, .F. ) ;
#9326=ADVANCED_FACE ( 'NONE', ( #712 ), #20048, .T. ) ;
#9372=ADVANCED_FACE ( 'NONE', ( #22255 ), #8937, .F. ) ;
#9378=CARTESIAN_POINT ( 'NONE',  ( 7.636616881710000193, 9.305349148710000406, 230.6412452697800006 ) ) ;
#9431=DIRECTION ( 'NONE',  ( 1.000000000000000000, 0.000000000000000000, 0.000000000000000000 ) ) ;
#9464=B_SPLINE_CURVE_WITH_KNOTS ( 'NONE', 3,
 ( #7361, #19477, #24051, #26559, #5000, #21531, #30971, #5310 ),
 .UNSPECIFIED., .F., .F.,
 ( 4, 2, 2, 4 ),
 ( 0.000000000000000000, 0.2500000000000000000, 0.5000000000000000000, 1.000000000000000000 ),
 .UNSPECIFIED. ) ;
#9490=DIRECTION ( 'NONE',  ( 0.9595496299847263710, -0.2815395311429191305, 0.000000000000000000 ) ) ;
#9496=CIRCLE ( 'NONE', #12013, 2.100000000000000089 ) ;
#9583=CARTESIAN_POINT ( 'NONE',  ( 1.064429457989999994, 12.07977735470000091, 230.6412452697800006 ) ) ;
#9659=CARTESIAN_POINT ( 'NONE',  ( 2.220446049249999755E-16, 2.100000000000000089, 226.6412452697800006 ) ) ;
#9672=PLANE ( 'NONE',  #28559 ) ;
#9674=CIRCLE ( 'NONE', #5646, 18.00000000000000000 ) ;
#9726=EDGE_LOOP ( 'NONE', ( #9950, #20742, #18604, #17101, #3992, #7519, #3431, #5825 ) ) ;
#9737=VECTOR ( 'NONE', #582, 1000.000000000000000 ) ;
#9774=CARTESIAN_POINT ( 'NONE',  ( 1.776356839399999804E-15, -5.329070518200000398E-15, 224.6412452697800290 ) ) ;
#9892=CARTESIAN_POINT ( 'NONE',  ( -2.525646774299999731, 11.92010449670000050, 230.6412452697800006 ) ) ;
#9895=EDGE_CURVE ( 'NONE', #23549, #19698, #10965, .T. ) ;
#9937=CARTESIAN_POINT ( 'NONE',  ( -4.352394000759999624E-10, -4.352376237189999857E-10, 227.6412452697800006 ) ) ;
#9950=ORIENTED_EDGE ( 'NONE', *, *, #15837, .F. ) ;
#9958=DIRECTION ( 'NONE',  ( 0.000000000000000000, 0.000000000000000000, 1.000000000000000000 ) ) ;
#9960=DIRECTION ( 'NONE',  ( 0.000000000000000000, 0.000000000000000000, 1.000000000000000000 ) ) ;
#9961=AXIS2_PLACEMENT_3D ( 'NONE', #10757, #3667, #29482 ) ;
#10023=VERTEX_POINT ( 'NONE', #2142 ) ;
#10036=VERTEX_POINT ( 'NONE', #28415 ) ;
#10068=CIRCLE ( 'NONE', #15573, 5.000000000000000000 ) ;
#10097=EDGE_LOOP ( 'NONE', ( #671, #15822, #22743, #26627, #27824 ) ) ;
#10103=CARTESIAN_POINT ( 'NONE',  ( 0.5496038886516223521, 2.045530029741057021, 226.6412452697799722 ) ) ;
#10143=CIRCLE ( 'NONE', #3588, 12.03781779390000040 ) ;
#10155=CARTESIAN_POINT ( 'NONE',  ( -3.389121577680000108, -11.55088360999999963, 224.6412452697800290 ) ) ;
#10196=CARTESIAN_POINT ( 'NONE',  ( 4.096142159599999388, 4.096142159599999388, 226.6412452697800006 ) ) ;
#10210=EDGE_CURVE ( 'NONE', #1959, #25501, #11914, .T. ) ;
#10226=ORIENTED_EDGE ( 'NONE', *, *, #10992, .T. ) ;
#10257=VERTEX_POINT ( 'NONE', #29174 ) ;
#10261=CARTESIAN_POINT ( 'NONE',  ( 7.636616881710000193, 9.305349148710000406, 230.6412452697800006 ) ) ;
#10368=CARTESIAN_POINT ( 'NONE',  ( -2.100000000000000089, -6.661338147749999512E-16, 226.6412452697800006 ) ) ;
#10395=CARTESIAN_POINT ( 'NONE',  ( 7.105427357599999217E-15, 8.881784197000000993E-16, 224.6412452697800290 ) ) ;
#10470=EDGE_CURVE ( 'NONE', #20819, #20463, #24975, .T. ) ;
#10524=ORIENTED_EDGE ( 'NONE', *, *, #14963, .F. ) ;
#10530=EDGE_CURVE ( 'NONE', #20819, #21014, #5874, .T. ) ;
#10550=CARTESIAN_POINT ( 'NONE',  ( 4.874695217780000256, -3.326860129179999959, 226.6412452697800006 ) ) ;
#10563=DIRECTION ( 'NONE',  ( 1.000000000000000000, 0.000000000000000000, 0.000000000000000000 ) ) ;
#10658=MANIFOLD_SOLID_BREP ( 'PartBody', #25633 ) ;
#10676=VERTEX_POINT ( 'NONE', #21260 ) ;
#10694=CARTESIAN_POINT ( 'NONE',  ( -4.884981308350000102E-15, -2.100000000000000089, 227.6412452697800006 ) ) ;
#10699=DIRECTION ( 'NONE',  ( -0.7071067811865475727, 0.7071067811865475727, 0.000000000000000000 ) ) ;
#10702=ORIENTED_EDGE ( 'NONE', *, *, #12468, .T. ) ;
#10724=AXIS2_PLACEMENT_3D ( 'NONE', #25664, #4255, #4407 ) ;
#10757=CARTESIAN_POINT ( 'NONE',  ( 0.000000000000000000, 0.000000000000000000, 229.6412452697800006 ) ) ;
#10832=CARTESIAN_POINT ( 'NONE',  ( -0.1392084988525406630, 2.100000000239999665, 226.6412452697800006 ) ) ;
#10947=CIRCLE ( 'NONE', #31055, 5.999999999999999112 ) ;
#10958=ORIENTED_EDGE ( 'NONE', *, *, #8448, .T. ) ;
#10965=CIRCLE ( 'NONE', #3936, 12.03781779370000038 ) ;
#10992=EDGE_CURVE ( 'NONE', #18650, #10676, #5388, .T. ) ;
#11013=CARTESIAN_POINT ( 'NONE',  ( 5.240471012820000496, 2.862882362300000150, 226.6412452697800006 ) ) ;
#11034=ORIENTED_EDGE ( 'NONE', *, *, #30380, .T. ) ;
#11155=LINE ( 'NONE', #26252, #7430 ) ;
#11181=ORIENTED_EDGE ( 'NONE', *, *, #458, .T. ) ;
#11187=EDGE_CURVE ( 'NONE', #15714, #10257, #16955, .T. ) ;
#11256=ORIENTED_EDGE ( 'NONE', *, *, #14423, .F. ) ;
#11276=AXIS2_PLACEMENT_3D ( 'NONE', #26845, #24797, #14897 ) ;
#11403=DIRECTION ( 'NONE',  ( 1.000000000000000000, 0.000000000000000000, 0.000000000000000000 ) ) ;
#11416=AXIS2_PLACEMENT_3D ( 'NONE', #24273, #9960, #2269 ) ;
#11448=CARTESIAN_POINT ( 'NONE',  ( 7.877322421339998826, -9.296057209400000687, 230.6412452697800006 ) ) ;
#11471=DIRECTION ( 'NONE',  ( 0.000000000000000000, 0.000000000000000000, 1.000000000000000000 ) ) ;
#11552=ORIENTED_EDGE ( 'NONE', *, *, #2143, .F. ) ;
#11585=CARTESIAN_POINT ( 'NONE',  ( -1.094484693600000114, 5.799375430310000468, 226.6412452697800006 ) ) ;
#11599=CARTESIAN_POINT ( 'NONE',  ( 4.792542393929999811, -11.13937006400000129, 230.6412452697800006 ) ) ;
#11621=TOROIDAL_SURFACE ( 'NONE', #2593, 12.03781779390000040, 5.000000000000000000 ) ;
#11690=ORIENTED_EDGE ( 'NONE', *, *, #17902, .F. ) ;
#11734=CARTESIAN_POINT ( 'NONE',  ( -2.862882362289999705, 5.240471012849999610, 226.6412452697800006 ) ) ;
#11817=EDGE_CURVE ( 'NONE', #9298, #7204, #11155, .T. ) ;
#11829=FACE_OUTER_BOUND ( 'NONE', #21842, .T. ) ;
#11841=VERTEX_POINT ( 'NONE', #30515 ) ;
#11847=( NAMED_UNIT ( * ) PLANE_ANGLE_UNIT ( ) SI_UNIT ( $, .RADIAN. ) );
#11862=CARTESIAN_POINT ( 'NONE',  ( -3.389121577140000063, -11.55088360979999962, 230.6412452697800006 ) ) ;
#11914=B_SPLINE_CURVE_WITH_KNOTS ( 'NONE', 3,
 ( #14718, #24159, #24309, #21651, #2600, #7473, #19282, #7325 ),
 .UNSPECIFIED., .F., .F.,
 ( 4, 2, 2, 4 ),
 ( 0.000000000000000000, 0.2499999999999998890, 0.4999999999999997780, 1.000000000000000000 ),
 .UNSPECIFIED. ) ;
#11926=CIRCLE ( 'NONE', #30003, 12.03781779370000038 ) ;
#11934=DIRECTION ( 'NONE',  ( 0.000000000000000000, 0.000000000000000000, 1.000000000000000000 ) ) ;
#11939=CARTESIAN_POINT ( 'NONE',  ( -12.09065967409999942, 0.9322763426430000777, 230.6412452697800006 ) ) ;
#11942=DIRECTION ( 'NONE',  ( 1.000000000000000000, 0.000000000000000000, 0.000000000000000000 ) ) ;
#11972=DIRECTION ( 'NONE',  ( 0.000000000000000000, 0.000000000000000000, 1.000000000000000000 ) ) ;
#11987=AXIS2_PLACEMENT_3D ( 'NONE', #7254, #23637, #21264 ) ;
#12013=AXIS2_PLACEMENT_3D ( 'NONE', #3886, #17715, #20561 ) ;
#12091=DIRECTION ( 'NONE',  ( -0.9595496299847263710, 0.2815395311429191305, 0.000000000000000000 ) ) ;
#12093=CARTESIAN_POINT ( 'NONE',  ( -9.954078586509998772, -7.027540153349999485, 230.6412452697800006 ) ) ;
#12144=ORIENTED_EDGE ( 'NONE', *, *, #30380, .F. ) ;
#12156=EDGE_CURVE ( 'NONE', #553, #16515, #21185, .T. ) ;
#12191=AXIS2_PLACEMENT_3D ( 'NONE', #1306, #17956, #27567 ) ;
#12217=CIRCLE ( 'NONE', #29797, 4.999999999999998224 ) ;
#12295=CARTESIAN_POINT ( 'NONE',  ( 0.000000000000000000, -1.776356839399999804E-15, 227.6412452697800006 ) ) ;
#12304=CARTESIAN_POINT ( 'NONE',  ( 7.636616881710000193, 9.305349148710000406, 230.6412452697800006 ) ) ;
#12409=CARTESIAN_POINT ( 'NONE',  ( -1.630907769230000026, -5.558498091359999727, 229.6412452697800006 ) ) ;
#12468=EDGE_CURVE ( 'NONE', #11841, #5428, #18931, .T. ) ;
#12491=EDGE_CURVE ( 'NONE', #10036, #4792, #20521, .T. ) ;
#12517=DIRECTION ( 'NONE',  ( 0.000000000000000000, 0.000000000000000000, 1.000000000000000000 ) ) ;
#12526=ADVANCED_FACE ( 'NONE', ( #19057 ), #1936, .T. ) ;
#12567=ORIENTED_EDGE ( 'NONE', *, *, #11187, .T. ) ;
#12714=CARTESIAN_POINT ( 'NONE',  ( -1.670464374220244963, 1.280497938789454837, 226.6412452697800290 ) ) ;
#12738=CARTESIAN_POINT ( 'NONE',  ( 7.105427357599999217E-15, 8.881784197000000993E-16, 228.3912452697800006 ) ) ;
#12830=ADVANCED_FACE ( 'NONE', ( #24666, #28924 ), #461, .F. ) ;
#12834=DIRECTION ( 'NONE',  ( 0.000000000000000000, 0.000000000000000000, 1.000000000000000000 ) ) ;
#12851=ORIENTED_EDGE ( 'NONE', *, *, #12893, .F. ) ;
#12853=VERTEX_POINT ( 'NONE', #2644 ) ;
#12869=DIRECTION ( 'NONE',  ( 0.6343890248118320141, 0.7730139489027949562, 0.000000000000000000 ) ) ;
#12878=ORIENTED_EDGE ( 'NONE', *, *, #18704, .T. ) ;
#12893=EDGE_CURVE ( 'NONE', #125, #14489, #9496, .T. ) ;
#12986=ORIENTED_EDGE ( 'NONE', *, *, #29676, .T. ) ;
#13052=DIRECTION ( 'NONE',  ( 0.000000000000000000, 0.000000000000000000, 1.000000000000000000 ) ) ;
#13063=LINE ( 'NONE', #3311, #29320 ) ;
#13116=CARTESIAN_POINT ( 'NONE',  ( 0.000000000000000000, -1.776356839399999804E-15, 227.6412452697800006 ) ) ;
#13216=AXIS2_PLACEMENT_3D ( 'NONE', #16200, #2204, #11942 ) ;
#13254=ORIENTED_EDGE ( 'NONE', *, *, #12491, .T. ) ;
#13364=CARTESIAN_POINT ( 'NONE',  ( 4.288653532660000600, -4.054393014039999521, 226.6412452697800006 ) ) ;
#13482=DIRECTION ( 'NONE',  ( 1.000000000000000000, 0.000000000000000000, 0.000000000000000000 ) ) ;
#13560=ORIENTED_EDGE ( 'NONE', *, *, #14423, .T. ) ;
#13664=VECTOR ( 'NONE', #16158, 1000.000000000000000 ) ;
#13765=FACE_OUTER_BOUND ( 'NONE', #24926, .T. ) ;
#13854=EDGE_LOOP ( 'NONE', ( #23805, #20940 ) ) ;
#13903=EDGE_LOOP ( 'NONE', ( #21333, #10958, #7724 ) ) ;
#13947=CARTESIAN_POINT ( 'NONE',  ( -5.799375405960000229, -1.094484689610000006, 226.6412452697800006 ) ) ;
#13955=CARTESIAN_POINT ( 'NONE',  ( 8.198872691879999995E-10, -3.797984149399999816E-10, 229.6412452697800006 ) ) ;
#13975=AXIS2_PLACEMENT_3D ( 'NONE', #27911, #26022, #59 ) ;
#13978=EDGE_LOOP ( 'NONE', ( #9323, #3657, #2645, #16238 ) ) ;
#13987=DIRECTION ( 'NONE',  ( 0.000000000000000000, 0.000000000000000000, 1.000000000000000000 ) ) ;
#14015=DIRECTION ( 'NONE',  ( 0.000000000000000000, 0.000000000000000000, 1.000000000000000000 ) ) ;
#14096=CARTESIAN_POINT ( 'NONE',  ( 5.480456702449999717, 10.74539518949999994, 230.6412452697800006 ) ) ;
#14215=CARTESIAN_POINT ( 'NONE',  ( 18.00000000000000000, -4.408582873759999616E-15, 229.6412452697800006 ) ) ;
#14219=B_SPLINE_CURVE_WITH_KNOTS ( 'NONE', 5,
 ( #1835, #1996, #21339, #11585, #11734, #14261, #16142, #28418, #30634, #13947, #6853, #2307, #25913, #30939, #1678 ),
 .UNSPECIFIED., .F., .F.,
 ( 6, 3, 3, 3, 6 ),
 ( 0.000000000000000000, 6.476076814690000738, 12.95215362940000325, 19.42823044409999866, 25.90430725880000651 ),
 .UNSPECIFIED. ) ;
#14252=FACE_OUTER_BOUND ( 'NONE', #1907, .T. ) ;
#14261=CARTESIAN_POINT ( 'NONE',  ( -4.288653532660000600, 4.054393014030000408, 226.6412452697800006 ) ) ;
#14291=EDGE_LOOP ( 'NONE', ( #28284, #1322, #5221, #7058 ) ) ;
#14391=DIRECTION ( 'NONE',  ( 0.000000000000000000, 0.000000000000000000, 1.000000000000000000 ) ) ;
#14423=EDGE_CURVE ( 'NONE', #4792, #23036, #21096, .T. ) ;
#14468=CARTESIAN_POINT ( 'NONE',  ( -4.198625225940000760, -11.29386252790000000, 230.6412452697800006 ) ) ;
#14489=VERTEX_POINT ( 'NONE', #24636 ) ;
#14511=DIRECTION ( 'NONE',  ( 1.000000000000000000, 0.000000000000000000, 0.000000000000000000 ) ) ;
#14525=EDGE_LOOP ( 'NONE', ( #8689, #27169, #11181, #3797, #12986, #23033, #19234, #15400 ) ) ;
#14611=CYLINDRICAL_SURFACE ( 'NONE', #16826, 2.100000000000000977 ) ;
#14633=DIRECTION ( 'NONE',  ( 0.000000000000000000, 0.000000000000000000, 1.000000000000000000 ) ) ;
#14677=CARTESIAN_POINT ( 'NONE',  ( 4.595672992649999955, 11.13819882230000147, 230.6412452697800006 ) ) ;
#14680=ORIENTED_EDGE ( 'NONE', *, *, #6408, .T. ) ;
#14698=ADVANCED_FACE ( 'NONE', ( #8561 ), #20692, .F. ) ;
#14718=CARTESIAN_POINT ( 'NONE',  ( -2.100000000000000089, -6.661338147749999512E-16, 226.6412452697800006 ) ) ;
#14743=CARTESIAN_POINT ( 'NONE',  ( -1.630907769230000026, -5.558498091359999727, 227.6412452697800006 ) ) ;
#14780=AXIS2_PLACEMENT_3D ( 'NONE', #8028, #26467, #17020 ) ;
#14785=VERTEX_POINT ( 'NONE', #4012 ) ;
#14823=ORIENTED_EDGE ( 'NONE', *, *, #10210, .F. ) ;
#14824=( GEOMETRIC_REPRESENTATION_CONTEXT ( 3 ) GLOBAL_UNCERTAINTY_ASSIGNED_CONTEXT ( ( #4965 ) ) GLOBAL_UNIT_ASSIGNED_CONTEXT ( ( #4773, #11847, #19238 ) ) REPRESENTATION_CONTEXT ( 'NONE', 'WORKASPACE' ) );
#14859=CARTESIAN_POINT ( 'NONE',  ( 1.998401444330000344E-15, 2.100000000000000089, 227.6412452697800006 ) ) ;
#14874=CARTESIAN_POINT ( 'NONE',  ( 0.000000000000000000, 0.000000000000000000, 229.6412452697800006 ) ) ;
#14897=DIRECTION ( 'NONE',  ( -0.2815395311429196301, -0.9595496299847262600, 0.000000000000000000 ) ) ;
#14963=EDGE_CURVE ( 'NONE', #2713, #28317, #30565, .T. ) ;
#14969=AXIS2_PLACEMENT_3D ( 'NONE', #3762, #11471, #20916 ) ;
#15025=VERTEX_POINT ( 'NONE', #14859 ) ;
#15084=CARTESIAN_POINT ( 'NONE',  ( -1.057731049208300078, 1.834980888704576207, 226.6412452697800575 ) ) ;
#15124=DIRECTION ( 'NONE',  ( 0.000000000000000000, 0.000000000000000000, 1.000000000000000000 ) ) ;
#15218=ORIENTED_EDGE ( 'NONE', *, *, #14963, .T. ) ;
#15273=DIRECTION ( 'NONE',  ( 0.000000000000000000, 0.000000000000000000, 1.000000000000000000 ) ) ;
#15274=EDGE_LOOP ( 'NONE', ( #19472, #6345, #13254, #13560 ) ) ;
#15277=ORIENTED_EDGE ( 'NONE', *, *, #1552, .F. ) ;
#15345=DIRECTION ( 'NONE',  ( 0.000000000000000000, 0.000000000000000000, 1.000000000000000000 ) ) ;
#15359=EDGE_CURVE ( 'NONE', #23036, #26756, #10947, .T. ) ;
#15385=CARTESIAN_POINT ( 'NONE',  ( -1.484924240490000047, 1.484924240490000047, 226.6412452697800006 ) ) ;
#15400=ORIENTED_EDGE ( 'NONE', *, *, #22144, .T. ) ;
#15405=CARTESIAN_POINT ( 'NONE',  ( 1.484924240490000047, -1.484924240490000047, 227.6412452697800006 ) ) ;
#15432=DIRECTION ( 'NONE',  ( 0.000000000000000000, 0.000000000000000000, 1.000000000000000000 ) ) ;
#15440=ORIENTED_EDGE ( 'NONE', *, *, #5479, .F. ) ;
#15449=CARTESIAN_POINT ( 'NONE',  ( 2.045342621092061552, -0.5496705570015011366, 226.6412452697799722 ) ) ;
#15573=AXIS2_PLACEMENT_3D ( 'NONE', #20681, #30444, #6664 ) ;
#15670=CARTESIAN_POINT ( 'NONE',  ( -1.484924240490000047, 1.484924240490000047, 226.6412452697800006 ) ) ;
#15686=PLANE ( 'NONE',  #6129 ) ;
#15714=VERTEX_POINT ( 'NONE', #6284 ) ;
#15743=ORIENTED_EDGE ( 'NONE', *, *, #21056, .F. ) ;
#15786=EDGE_LOOP ( 'NONE', ( #22484, #30182 ) ) ;
#15813=PRODUCT_DEFINITION ( 'UNKNOWN', '', #20381, #17836 ) ;
#15822=ORIENTED_EDGE ( 'NONE', *, *, #18704, .F. ) ;
#15837=EDGE_CURVE ( 'NONE', #10676, #16947, #15997, .T. ) ;
#15950=CARTESIAN_POINT ( 'NONE',  ( 1.290548111051992519, -1.679300369702346085, 226.6412452697800006 ) ) ;
#15997=CIRCLE ( 'NONE', #3426, 2.100000000000000089 ) ;
#16038=CARTESIAN_POINT ( 'NONE',  ( -2.100000000000000089, 2.220446049249999755E-16, 227.6412452697800006 ) ) ;
#16060=ORIENTED_EDGE ( 'NONE', *, *, #9895, .F. ) ;
#16142=CARTESIAN_POINT ( 'NONE',  ( -4.874695217770000255, 3.326860129169999958, 226.6412452697800006 ) ) ;
#16144=DIRECTION ( 'NONE',  ( 0.000000000000000000, 0.000000000000000000, 1.000000000000000000 ) ) ;
#16150=ORIENTED_EDGE ( 'NONE', *, *, #8448, .F. ) ;
#16158=DIRECTION ( 'NONE',  ( 0.000000000000000000, 0.000000000000000000, 1.000000000000000000 ) ) ;
#16159=CARTESIAN_POINT ( 'NONE',  ( 9.051856682629999540, 7.975114694340000199, 230.6412452697800006 ) ) ;
#16200=CARTESIAN_POINT ( 'NONE',  ( 0.000000000000000000, 0.000000000000000000, 230.6412452697800006 ) ) ;
#16238=ORIENTED_EDGE ( 'NONE', *, *, #21056, .T. ) ;
#16241=CARTESIAN_POINT ( 'NONE',  ( -1.386473475049334159, -1.583312407435810254, 226.6412452697799722 ) ) ;
#16316=CARTESIAN_POINT ( 'NONE',  ( 8.609713997930001028, 8.450495286409998030, 230.6412452697800006 ) ) ;
#16440=ORIENTED_EDGE ( 'NONE', *, *, #3929, .F. ) ;
#16479=EDGE_CURVE ( 'NONE', #10036, #26756, #9160, .T. ) ;
#16504=AXIS2_PLACEMENT_3D ( 'NONE', #4101, #2216, #1749 ) ;
#16515=VERTEX_POINT ( 'NONE', #29004 ) ;
#16526=DIRECTION ( 'NONE',  ( 0.000000000000000000, 0.000000000000000000, 1.000000000000000000 ) ) ;
#16559=VERTEX_POINT ( 'NONE', #7900 ) ;
#16561=( NAMED_UNIT ( * ) PLANE_ANGLE_UNIT ( ) SI_UNIT ( $, .RADIAN. ) );
#16563=B_SPLINE_CURVE_WITH_KNOTS ( 'NONE', 3,
 ( #23501, #16241, #19502, #23654, #16976, #24217, #30726, #21280 ),
 .UNSPECIFIED., .F., .F.,
 ( 4, 2, 2, 4 ),
 ( 0.000000000000000000, 0.2499999999999998890, 0.4999999999999997780, 1.000000000000000000 ),
 .UNSPECIFIED. ) ;
#16595=CARTESIAN_POINT ( 'NONE',  ( 3.796508223180000030, 11.43135311160000001, 230.6412452697800006 ) ) ;
#16750=CIRCLE ( 'NONE', #3185, 2.999999999999997780 ) ;
#16819=CARTESIAN_POINT ( 'NONE',  ( 4.096142159599999388, 4.096142159599999388, 227.6412452697800006 ) ) ;
#16826=AXIS2_PLACEMENT_3D ( 'NONE', #5461, #7364, #7660 ) ;
#16938=AXIS2_PLACEMENT_3D ( 'NONE', #3363, #3058, #5879 ) ;
#16947=VERTEX_POINT ( 'NONE', #10694 ) ;
#16955=CIRCLE ( 'NONE', #4406, 1.999999999999999112 ) ;
#16967=CARTESIAN_POINT ( 'NONE',  ( -6.072586508529999705, -10.48251654620000117, 230.6412452697800006 ) ) ;
#16975=FACE_OUTER_BOUND ( 'NONE', #15786, .T. ) ;
#16976=CARTESIAN_POINT ( 'NONE',  ( -0.9307262390600369306, -1.887507901406886957, 226.6412452697800006 ) ) ;
#16981=AXIS2_PLACEMENT_3D ( 'NONE', #19262, #81, #7453 ) ;
#17020=DIRECTION ( 'NONE',  ( 1.000000000000000000, 0.000000000000000000, 0.000000000000000000 ) ) ;
#17083=DIRECTION ( 'NONE',  ( 1.000000000000000000, 0.000000000000000000, 0.000000000000000000 ) ) ;
#17096=EDGE_CURVE ( 'NONE', #21014, #5533, #17218, .T. ) ;
#17101=ORIENTED_EDGE ( 'NONE', *, *, #7485, .F. ) ;
#17103=DIRECTION ( 'NONE',  ( 0.000000000000000000, 0.000000000000000000, 1.000000000000000000 ) ) ;
#17113=DIRECTION ( 'NONE',  ( 1.000000000000000000, 0.000000000000000000, 0.000000000000000000 ) ) ;
#17121=CARTESIAN_POINT ( 'NONE',  ( -1.630907768819999992, -5.558498092260000689, 226.6412452697800006 ) ) ;
#17126=PLANE ( 'NONE',  #19837 ) ;
#17164=CARTESIAN_POINT ( 'NONE',  ( 7.105427357599999217E-15, 8.881784197000000993E-16, 224.6412452697800290 ) ) ;
#17218=B_SPLINE_CURVE_WITH_KNOTS ( 'NONE', 5,
 ( #30043, #22811, #1263, #27677, #27837, #13364, #10550, #22974, #6123, #1419, #11013, #30201, #28893, #18398, #4085 ),
 .UNSPECIFIED., .F., .F.,
 ( 6, 3, 3, 3, 6 ),
 ( 0.000000000000000000, 6.476076814690000738, 12.95215362940000325, 19.42823044409999866, 25.90430725880000651 ),
 .UNSPECIFIED. ) ;
#17274=CARTESIAN_POINT ( 'NONE',  ( -7.877322421349998827, 9.296057209389999798, 230.6412452697800006 ) ) ;
#17331=CARTESIAN_POINT ( 'NONE',  ( 0.2762902770302890221, 2.100000000240000109, 226.6412452697799438 ) ) ;
#17369=DIRECTION ( 'NONE',  ( 0.7071067811865475727, -0.7071067811865475727, 0.000000000000000000 ) ) ;
#17391=LINE ( 'NONE', #22122, #9737 ) ;
#17407=VERTEX_POINT ( 'NONE', #9659 ) ;
#17428=ADVANCED_BREP_SHAPE_REPRESENTATION ( '', ( #10658, #17722 ), #14824 ) ;
#17437=CARTESIAN_POINT ( 'NONE',  ( -1.484924240490000047, 1.484924240490000047, 226.6412452697800006 ) ) ;
#17591=EDGE_CURVE ( 'NONE', #26756, #15714, #20738, .T. ) ;
#17621=CYLINDRICAL_SURFACE ( 'NONE', #27865, 2.100000000000000977 ) ;
#17673=DIRECTION ( 'NONE',  ( 0.000000000000000000, 0.000000000000000000, 1.000000000000000000 ) ) ;
#17715=DIRECTION ( 'NONE',  ( 0.000000000000000000, 0.000000000000000000, -1.000000000000000000 ) ) ;
#17722=AXIS2_PLACEMENT_3D ( 'NONE', #2627, #14015, #29203 ) ;
#17742=AXIS2_PLACEMENT_3D ( 'NONE', #20159, #15432, #10563 ) ;
#17776=ORIENTED_EDGE ( 'NONE', *, *, #7485, .T. ) ;
#17793=SURFACE_STYLE_USAGE ( .BOTH. , #30077 ) ;
#17836=PRODUCT_DEFINITION_CONTEXT ( 'detailed design', #24645, 'design' ) ;
#17902=EDGE_CURVE ( 'NONE', #25445, #10257, #9201, .T. ) ;
#17933=ADVANCED_FACE ( 'NONE', ( #24250 ), #2697, .F. ) ;
#17956=DIRECTION ( 'NONE',  ( 0.000000000000000000, 0.000000000000000000, 1.000000000000000000 ) ) ;
#17967=VECTOR ( 'NONE', #30899, 1000.000000000000000 ) ;
#18038=DIRECTION ( 'NONE',  ( 0.000000000000000000, 0.000000000000000000, 1.000000000000000000 ) ) ;
#18058=ORIENTED_EDGE ( 'NONE', *, *, #11817, .T. ) ;
#18082=EDGE_CURVE ( 'NONE', #28317, #2713, #25802, .T. ) ;
#18160=CARTESIAN_POINT ( 'NONE',  ( -8.881784197000000993E-16, -8.881784197000000993E-16, 227.6412452697800006 ) ) ;
#18275=EDGE_CURVE ( 'NONE', #14489, #16947, #21775, .T. ) ;
#18384=ORIENTED_EDGE ( 'NONE', *, *, #26028, .T. ) ;
#18385=EDGE_CURVE ( 'NONE', #10023, #20819, #12217, .T. ) ;
#18398=CARTESIAN_POINT ( 'NONE',  ( 2.504034607669999968, 5.302315698040000136, 226.6412452697800006 ) ) ;
#18455=EDGE_LOOP ( 'NONE', ( #15277, #11256, #15743 ) ) ;
#18456=ORIENTED_EDGE ( 'NONE', *, *, #22144, .F. ) ;
#18461=CARTESIAN_POINT ( 'NONE',  ( 0.2748893566200901750, -2.100000000056975402, 226.6412452697800290 ) ) ;
#18519=CARTESIAN_POINT ( 'NONE',  ( 11.93900533800000119, -2.124654349530000097, 230.6412452697800006 ) ) ;
#18536=PRODUCT_CONTEXT ( 'NONE', #6954, 'mechanical' ) ;
#18560=EDGE_CURVE ( 'NONE', #15714, #10036, #22288, .T. ) ;
#18604=ORIENTED_EDGE ( 'NONE', *, *, #25859, .F. ) ;
#18650=VERTEX_POINT ( 'NONE', #16038 ) ;
#18670=CARTESIAN_POINT ( 'NONE',  ( 5.871915332789999553, -10.61013173299999934, 230.6412452697800006 ) ) ;
#18682=EDGE_LOOP ( 'NONE', ( #12851, #28610, #10702, #26011 ) ) ;
#18704=EDGE_CURVE ( 'NONE', #5036, #5533, #16750, .T. ) ;
#18718=CYLINDRICAL_SURFACE ( 'NONE', #30342, 2.100000000000000977 ) ;
#18829=CARTESIAN_POINT ( 'NONE',  ( 12.09628639090000135, 1.465387503880000164, 230.6412452697800006 ) ) ;
#18831=MECHANICAL_DESIGN_GEOMETRIC_PRESENTATION_REPRESENTATION('',(#25377),#22855);
#18925=( LENGTH_UNIT ( ) NAMED_UNIT ( * ) SI_UNIT ( .MILLI., .METRE. ) );
#18931=B_SPLINE_CURVE_WITH_KNOTS ( 'NONE', 3,
 ( #27408, #5846, #15449, #30, #19212, #6940 ),
 .UNSPECIFIED., .F., .F.,
 ( 4, 2, 4 ),
 ( 0.000000000000000000, 0.5000000000000002220, 1.000000000000000000 ),
 .UNSPECIFIED. ) ;
#18960=CARTESIAN_POINT ( 'NONE',  ( 6.778377084329999747, 9.970142431730000254, 230.6412452697800006 ) ) ;
#19018=EDGE_CURVE ( 'NONE', #25501, #10676, #25458, .T. ) ;
#19057=FACE_OUTER_BOUND ( 'NONE', #15274, .T. ) ;
#19138=ORIENTED_EDGE ( 'NONE', *, *, #1001, .T. ) ;
#19170=FACE_OUTER_BOUND ( 'NONE', #3408, .T. ) ;
#19180=CARTESIAN_POINT ( 'NONE',  ( -3.796508279279999787, -11.43135309280000023, 230.6412452697800006 ) ) ;
#19198=EDGE_CURVE ( 'NONE', #19698, #10023, #10143, .T. ) ;
#19212=CARTESIAN_POINT ( 'NONE',  ( 1.679300368525225240, -1.290548112687445181, 226.6412452697799438 ) ) ;
#19234=ORIENTED_EDGE ( 'NONE', *, *, #10210, .T. ) ;
#19238=( NAMED_UNIT ( * ) SI_UNIT ( $, .STERADIAN. ) SOLID_ANGLE_UNIT ( ) );
#19262=CARTESIAN_POINT ( 'NONE',  ( 0.000000000000000000, 0.000000000000000000, 230.6412452697800006 ) ) ;
#19282=CARTESIAN_POINT ( 'NONE',  ( -1.680165883105034119, -1.289604809122433915, 226.6412452697800859 ) ) ;
#19320=CIRCLE ( 'NONE', #17742, 8.134694044909998922 ) ;
#19341=CARTESIAN_POINT ( 'NONE',  ( 3.389121577140000063, 11.55088360979999962, 230.6412452697800006 ) ) ;
#19344=DIRECTION ( 'NONE',  ( 0.000000000000000000, 0.000000000000000000, 1.000000000000000000 ) ) ;
#19362=ORIENTED_EDGE ( 'NONE', *, *, #29676, .F. ) ;
#19385=DIRECTION ( 'NONE',  ( 0.000000000000000000, 0.000000000000000000, 1.000000000000000000 ) ) ;
#19396=EDGE_LOOP ( 'NONE', ( #9089, #21405, #20616, #7966 ) ) ;
#19472=ORIENTED_EDGE ( 'NONE', *, *, #15359, .T. ) ;
#19477=CARTESIAN_POINT ( 'NONE',  ( 2.100000000239999665, 0.1392085007613527159, 226.6412452697800006 ) ) ;
#19502=CARTESIAN_POINT ( 'NONE',  ( -1.280497936623963495, -1.670464374936807328, 226.6412452697800290 ) ) ;
#19516=CARTESIAN_POINT ( 'NONE',  ( 8.198872691879999995E-10, -3.797984149399999816E-10, 229.6412452697800006 ) ) ;
#19517=ORIENTED_EDGE ( 'NONE', *, *, #2143, .T. ) ;
#19558=DIRECTION ( 'NONE',  ( 0.7071067811865475727, 0.7071067811865475727, 0.000000000000000000 ) ) ;
#19654=DIRECTION ( 'NONE',  ( 0.000000000000000000, 0.000000000000000000, 1.000000000000000000 ) ) ;
#19682=CARTESIAN_POINT ( 'NONE',  ( -1.776356839399999804E-15, -1.776356839399999804E-15, 229.6412452697800006 ) ) ;
#19698=VERTEX_POINT ( 'NONE', #5324 ) ;
#19837=AXIS2_PLACEMENT_3D ( 'NONE', #16819, #19654, #26580 ) ;
#19844=ADVANCED_FACE ( 'NONE', ( #1696, #27808 ), #15686, .T. ) ;
#19852=FACE_OUTER_BOUND ( 'NONE', #29603, .T. ) ;
#19861=CARTESIAN_POINT ( 'NONE',  ( 2.220446049249999755E-16, 2.100000000000000089, 226.6412452697800006 ) ) ;
#19864=CARTESIAN_POINT ( 'NONE',  ( 7.217190561760000733, 9.649559097600000968, 230.6412452697800006 ) ) ;
#19921=DIRECTION ( 'NONE',  ( 1.000000000000000000, 0.000000000000000000, 0.000000000000000000 ) ) ;
#19956=CARTESIAN_POINT ( 'NONE',  ( -1.289604807081810911, 1.680165884098436591, 226.6412452697800006 ) ) ;
#20000=B_SPLINE_CURVE_WITH_KNOTS ( 'NONE', 5,
 ( #19341, #5159, #9583, #21396, #9892, #26721, #28931, #17274, #313, #29231, #30987, #2810, #11939, #26266, #7375, #7221, #12093, #23920, #4705, #16967, #4553, #14468, #19180, #26574 ),
 .UNSPECIFIED., .F., .F.,
 ( 6, 3, 3, 3, 3, 3, 3, 6 ),
 ( 0.000000000000000000, 8.467772783510000068, 16.93507402379999860, 25.40292880670000031, 33.87083985900000016, 42.33863182010000514, 50.80649256519998858, 53.82812356579999857 ),
 .UNSPECIFIED. ) ;
#20048=CYLINDRICAL_SURFACE ( 'NONE', #9961, 18.00000000000000000 ) ;
#20115=DIRECTION ( 'NONE',  ( 1.000000000000000000, 0.000000000000000000, 0.000000000000000000 ) ) ;
#20159=CARTESIAN_POINT ( 'NONE',  ( 1.776356839399999804E-15, -5.329070518200000398E-15, 227.7662452697800006 ) ) ;
#20163=ORIENTED_EDGE ( 'NONE', *, *, #18082, .F. ) ;
#20364=DIRECTION ( 'NONE',  ( -0.9595496299849965993, 0.2815395311419987001, 0.000000000000000000 ) ) ;
#20381=PRODUCT_DEFINITION_FORMATION_WITH_SPECIFIED_SOURCE ( 'ANY', '', #4122, .NOT_KNOWN. ) ;
#20463=VERTEX_POINT ( 'NONE', #1605 ) ;
#20473=FILL_AREA_STYLE_COLOUR ( '', #24491 ) ;
#20521=CIRCLE ( 'NONE', #11987, 6.000000000000000000 ) ;
#20561=DIRECTION ( 'NONE',  ( 1.000000000000000000, 0.000000000000000000, 0.000000000000000000 ) ) ;
#20576=CARTESIAN_POINT ( 'NONE',  ( -0.6766242627705201240, 1.992768275178435911, 226.6412452697800006 ) ) ;
#20616=ORIENTED_EDGE ( 'NONE', *, *, #879, .F. ) ;
#20681=CARTESIAN_POINT ( 'NONE',  ( 7.636659491129999644, 9.305401069029999306, 224.6412452697800290 ) ) ;
#20692=CYLINDRICAL_SURFACE ( 'NONE', #30390, 2.100000000000000977 ) ;
#20718=CARTESIAN_POINT ( 'NONE',  ( -1.484924240490000047, 1.484924240490000047, 227.6412452697800006 ) ) ;
#20738=CIRCLE ( 'NONE', #12191, 7.354069295110000404 ) ;
#20742=ORIENTED_EDGE ( 'NONE', *, *, #10992, .F. ) ;
#20791=( NAMED_UNIT ( * ) PLANE_ANGLE_UNIT ( ) SI_UNIT ( $, .RADIAN. ) );
#20819=VERTEX_POINT ( 'NONE', #24412 ) ;
#20859=B_SPLINE_CURVE_WITH_KNOTS ( 'NONE', 3,
 ( #17437, #27652, #12714, #5480, #7834, #8136, #25144, #10368 ),
 .UNSPECIFIED., .F., .F.,
 ( 4, 2, 2, 4 ),
 ( 0.000000000000000000, 0.2499999999999999445, 0.4999999999999998890, 1.000000000000000000 ),
 .UNSPECIFIED. ) ;
#20862=DIRECTION ( 'NONE',  ( -1.000000000000000000, 1.224646799149999589E-16, 0.000000000000000000 ) ) ;
#20916=DIRECTION ( 'NONE',  ( 1.000000000000000000, 0.000000000000000000, 0.000000000000000000 ) ) ;
#20940=ORIENTED_EDGE ( 'NONE', *, *, #7167, .F. ) ;
#21014=VERTEX_POINT ( 'NONE', #17121 ) ;
#21048=CARTESIAN_POINT ( 'NONE',  ( 0.1368966849300000121, -12.12573834550000029, 230.6412452697800006 ) ) ;
#21056=EDGE_CURVE ( 'NONE', #12853, #4792, #20000, .T. ) ;
#21096=B_SPLINE_CURVE_WITH_KNOTS ( 'NONE', 5,
 ( #2009, #21197, #9075, #21048, #30648, #11599, #18670, #11448, #30795, #21356, #28432, #18519, #28121, #18829, #7183, #6866, #28272, #16159, #16316, #8918, #9378 ),
 .UNSPECIFIED., .F., .F.,
 ( 6, 3, 3, 3, 3, 3, 6 ),
 ( 0.000000000000000000, 8.467772783080000920, 16.93507402329999678, 25.40292880620000204, 33.87083985430000155, 42.33863182420000015, 46.94504270979999916 ),
 .UNSPECIFIED. ) ;
#21159=ADVANCED_FACE ( 'NONE', ( #2962 ), #11621, .F. ) ;
#21172=CARTESIAN_POINT ( 'NONE',  ( 6.321956670630000552, 10.26563848810000046, 230.6412452697800006 ) ) ;
#21185=LINE ( 'NONE', #20718, #26061 ) ;
#21197=CARTESIAN_POINT ( 'NONE',  ( -2.247467472309999437, -11.88585404939999890, 230.6412452697800006 ) ) ;
#21260=CARTESIAN_POINT ( 'NONE',  ( -1.484924240490000047, -1.484924240490000047, 227.6412452697800006 ) ) ;
#21264=DIRECTION ( 'NONE',  ( 0.2815395369041025497, 0.9595496282943490884, 0.000000000000000000 ) ) ;
#21280=CARTESIAN_POINT ( 'NONE',  ( -4.884981308350000102E-15, -2.100000000000000089, 226.6412452697800006 ) ) ;
#21297=AXIS2_PLACEMENT_3D ( 'NONE', #17164, #19385, #28975 ) ;
#21333=ORIENTED_EDGE ( 'NONE', *, *, #19198, .T. ) ;
#21339=CARTESIAN_POINT ( 'NONE',  ( -0.1656472034169999830, 5.899424820049999241, 226.6412452697800006 ) ) ;
#21356=CARTESIAN_POINT ( 'NONE',  ( 10.20188979230000115, -6.555481593089999670, 230.6412452697800006 ) ) ;
#21377=AXIS2_PLACEMENT_3D ( 'NONE', #9774, #4582, #28966 ) ;
#21396=CARTESIAN_POINT ( 'NONE',  ( -0.1368966847449999968, 12.12573834550000029, 230.6412452697800006 ) ) ;
#21405=ORIENTED_EDGE ( 'NONE', *, *, #1552, .T. ) ;
#21448=ORIENTED_EDGE ( 'NONE', *, *, #28630, .F. ) ;
#21449=SURFACE_STYLE_FILL_AREA ( #2711 ) ;
#21503=AXIS2_PLACEMENT_3D ( 'NONE', #24617, #5564, #861 ) ;
#21531=CARTESIAN_POINT ( 'NONE',  ( 1.834980886315526805, 1.057731052269877070, 226.6412452697800575 ) ) ;
#21588=ADVANCED_FACE ( 'NONE', ( #27157 ), #27840, .F. ) ;
#21600=CIRCLE ( 'NONE', #25092, 2.100000000000000089 ) ;
#21636=DIRECTION ( 'NONE',  ( 0.000000000000000000, 0.000000000000000000, 1.000000000000000000 ) ) ;
#21651=CARTESIAN_POINT ( 'NONE',  ( -2.033405199220553516, -0.5436710271403359940, 226.6412452697799154 ) ) ;
#21699=CARTESIAN_POINT ( 'NONE',  ( 1.630907769230000026, 5.558498091359999727, 229.6412452697800006 ) ) ;
#21742=FACE_OUTER_BOUND ( 'NONE', #13978, .T. ) ;
#21760=EDGE_CURVE ( 'NONE', #7767, #2713, #7312, .T. ) ;
#21775=CIRCLE ( 'NONE', #23280, 2.100000000000000089 ) ;
#21842=EDGE_LOOP ( 'NONE', ( #16150, #6651, #3243, #25978 ) ) ;
#21953=CARTESIAN_POINT ( 'NONE',  ( 0.000000000000000000, -1.776356839399999804E-15, 227.6412452697800006 ) ) ;
#22067=CARTESIAN_POINT ( 'NONE',  ( 1.053429626907578687, 1.822228222601957714, 226.6412452697800290 ) ) ;
#22122=CARTESIAN_POINT ( 'NONE',  ( -2.100000000000000089, -1.554312234479999851E-15, 227.6412452697800006 ) ) ;
#22123=CARTESIAN_POINT ( 'NONE',  ( 7.105427357599999217E-15, 8.881784197000000993E-16, 229.6412452697800006 ) ) ;
#22144=EDGE_CURVE ( 'NONE', #25501, #16559, #16563, .T. ) ;
#22193=ORIENTED_EDGE ( 'NONE', *, *, #25681, .T. ) ;
#22255=FACE_OUTER_BOUND ( 'NONE', #25540, .T. ) ;
#22288=CIRCLE ( 'NONE', #26315, 7.354069295110000404 ) ;
#22325=CIRCLE ( 'NONE', #14780, 8.134694044909998922 ) ;
#22484=ORIENTED_EDGE ( 'NONE', *, *, #28630, .T. ) ;
#22508=B_SPLINE_CURVE_WITH_KNOTS ( 'NONE', 3,
 ( #1488, #15950, #8859, #3668, #18461, #30439 ),
 .UNSPECIFIED., .F., .F.,
 ( 4, 2, 4 ),
 ( 0.000000000000000000, 0.5000000000000000000, 1.000000000000000000 ),
 .UNSPECIFIED. ) ;
#22521=EDGE_LOOP ( 'NONE', ( #8185, #15218 ) ) ;
#22631=CARTESIAN_POINT ( 'NONE',  ( -0.5436710233579141738, 2.033405200009645863, 226.6412452697799438 ) ) ;
#22718=CARTESIAN_POINT ( 'NONE',  ( 1.484924240490000047, 1.484924240490000047, 226.6412452697800006 ) ) ;
#22725=DIRECTION ( 'NONE',  ( 1.000000000000000000, 0.000000000000000000, 0.000000000000000000 ) ) ;
#22743=ORIENTED_EDGE ( 'NONE', *, *, #30860, .F. ) ;
#22811=CARTESIAN_POINT ( 'NONE',  ( -0.7577809307819999285, -5.814680484680000205, 226.6412452697800006 ) ) ;
#22855=( GEOMETRIC_REPRESENTATION_CONTEXT ( 3 ) GLOBAL_UNCERTAINTY_ASSIGNED_CONTEXT ( ( #8084 ) ) GLOBAL_UNIT_ASSIGNED_CONTEXT ( ( #18925, #16561, #2560 ) ) REPRESENTATION_CONTEXT ( 'NONE', 'WORKASPACE' ) );
#22974=CARTESIAN_POINT ( 'NONE',  ( 5.729936103070000009, -1.681209052119999825, 226.6412452697800006 ) ) ;
#23033=ORIENTED_EDGE ( 'NONE', *, *, #26186, .T. ) ;
#23034=EDGE_CURVE ( 'NONE', #9298, #17407, #27368, .T. ) ;
#23036=VERTEX_POINT ( 'NONE', #12304 ) ;
#23043=FACE_OUTER_BOUND ( 'NONE', #18682, .T. ) ;
#23280=AXIS2_PLACEMENT_3D ( 'NONE', #1073, #8131, #20115 ) ;
#23307=ORIENTED_EDGE ( 'NONE', *, *, #5479, .T. ) ;
#23309=ADVANCED_FACE ( 'NONE', ( #2053 ), #18718, .F. ) ;
#23310=ORIENTED_EDGE ( 'NONE', *, *, #2639, .T. ) ;
#23386=CARTESIAN_POINT ( 'NONE',  ( 0.000000000000000000, 0.000000000000000000, 229.6412452697800006 ) ) ;
#23387=CARTESIAN_POINT ( 'NONE',  ( 0.000000000000000000, 0.000000000000000000, 229.6412452697800006 ) ) ;
#23501=CARTESIAN_POINT ( 'NONE',  ( -1.484924240490000047, -1.484924240490000047, 226.6412452697800006 ) ) ;
#23549=VERTEX_POINT ( 'NONE', #26534 ) ;
#23592=EDGE_CURVE ( 'NONE', #1959, #18650, #17391, .T. ) ;
#23607=TOROIDAL_SURFACE ( 'NONE', #9007, 5.792819795519999815, 3.000000000000000000 ) ;
#23627=AXIS2_PLACEMENT_3D ( 'NONE', #4650, #2146, #4188 ) ;
#23637=DIRECTION ( 'NONE',  ( 0.9595496282943491995, -0.2815395369041025497, 0.000000000000000000 ) ) ;
#23638=ORIENTED_EDGE ( 'NONE', *, *, #18560, .T. ) ;
#23654=CARTESIAN_POINT ( 'NONE',  ( -1.053429623273372640, -1.822228224019613485, 226.6412452697799154 ) ) ;
#23667=LINE ( 'NONE', #14215, #17967 ) ;
#23699=CARTESIAN_POINT ( 'NONE',  ( 3.389121577140000063, 11.55088360979999962, 230.6412452697800006 ) ) ;
#23805=ORIENTED_EDGE ( 'NONE', *, *, #17096, .F. ) ;
#23863=CARTESIAN_POINT ( 'NONE',  ( 1.484924240490000047, 1.484924240490000047, 227.6412452697800006 ) ) ;
#23866=CIRCLE ( 'NONE', #4250, 18.00000000000000000 ) ;
#23920=CARTESIAN_POINT ( 'NONE',  ( -8.341448913149999811, -8.801865131599999614, 230.6412452697800006 ) ) ;
#23989=CIRCLE ( 'NONE', #7395, 5.999999999999996447 ) ;
#24045=EDGE_LOOP ( 'NONE', ( #23307, #2155, #20163, #19517 ) ) ;
#24051=CARTESIAN_POINT ( 'NONE',  ( 2.086681040044585433, 0.2757844057790842518, 226.6412452697800290 ) ) ;
#24065=DIRECTION ( 'NONE',  ( 0.2815395311429192970, 0.9595496299847263710, 0.000000000000000000 ) ) ;
#24074=ADVANCED_FACE ( 'NONE', ( #13765 ), #8881, .T. ) ;
#24078=CARTESIAN_POINT ( 'NONE',  ( 1.776356839399999804E-15, 1.776356839399999804E-15, 229.6412452697800006 ) ) ;
#24159=CARTESIAN_POINT ( 'NONE',  ( -2.099999999790000960, -0.1392085008781404898, 226.6412452697799722 ) ) ;
#24217=CARTESIAN_POINT ( 'NONE',  ( -0.5496038873989572693, -2.045530029857146825, 226.6412452697800006 ) ) ;
#24231=DIRECTION ( 'NONE',  ( 1.000000000000000000, 0.000000000000000000, 0.000000000000000000 ) ) ;
#24250=FACE_OUTER_BOUND ( 'NONE', #30258, .T. ) ;
#24273=CARTESIAN_POINT ( 'NONE',  ( 1.776356839399999804E-15, -5.329070518200000398E-15, 227.7662452697800006 ) ) ;
#24309=CARTESIAN_POINT ( 'NONE',  ( -2.086681039676111737, -0.2757844063077397601, 226.6412452697800290 ) ) ;
#24412=CARTESIAN_POINT ( 'NONE',  ( -2.290237947390000084, -7.805642660830000246, 227.7662452697800006 ) ) ;
#24467=DIRECTION ( 'NONE',  ( 0.000000000000000000, 0.000000000000000000, 1.000000000000000000 ) ) ;
#24491=COLOUR_RGB ( '', 0.40784314, 0.44705882, 0.49803922) ;
#24617=CARTESIAN_POINT ( 'NONE',  ( 0.000000000000000000, 0.000000000000000000, 229.6412452697800006 ) ) ;
#24636=CARTESIAN_POINT ( 'NONE',  ( 1.484924240490000047, -1.484924240490000047, 227.6412452697800006 ) ) ;
#24645=APPLICATION_CONTEXT ( 'automotive_design' ) ;
#24666=FACE_BOUND ( 'NONE', #14525, .T. ) ;
#24680=CARTESIAN_POINT ( 'NONE',  ( -0.2757844036473713900, 2.086681040193929082, 226.6412452697800290 ) ) ;
#24763=ADVANCED_FACE ( 'NONE', ( #19852 ), #17621, .F. ) ;
#24779=DIRECTION ( 'NONE',  ( 0.2815395311419987556, 0.9595496299849963773, 0.000000000000000000 ) ) ;
#24797=DIRECTION ( 'NONE',  ( 0.000000000000000000, 0.000000000000000000, 1.000000000000000000 ) ) ;
#24902=TOROIDAL_SURFACE ( 'NONE', #21377, 12.03781779390000040, 5.000000000000000000 ) ;
#24926=EDGE_LOOP ( 'NONE', ( #26474, #11552, #10524, #7274 ) ) ;
#24968=CARTESIAN_POINT ( 'NONE',  ( 1.630907769230000026, 5.558498091359999727, 229.6412452697800006 ) ) ;
#24975=CIRCLE ( 'NONE', #11416, 8.134694044909998922 ) ;
#25000=TOROIDAL_SURFACE ( 'NONE', #6407, 12.03781779390000040, 6.000000000000000000 ) ;
#25030=ADVANCED_FACE ( 'NONE', ( #29089, #16975 ), #17126, .T. ) ;
#25081=CARTESIAN_POINT ( 'NONE',  ( -2.100000000000000089, -6.661338147749999512E-16, 226.6412452697800006 ) ) ;
#25084=AXIS2_PLACEMENT_3D ( 'NONE', #10196, #7518, #17113 ) ;
#25092=AXIS2_PLACEMENT_3D ( 'NONE', #13116, #17673, #22725 ) ;
#25144=CARTESIAN_POINT ( 'NONE',  ( -2.099999999790000960, 0.2762902854420857257, 226.6412452697799722 ) ) ;
#25173=FACE_OUTER_BOUND ( 'NONE', #8691, .T. ) ;
#25207=CARTESIAN_POINT ( 'NONE',  ( 2.290237947399999641, 7.805642660830000246, 227.7662452697800006 ) ) ;
#25248=DIRECTION ( 'NONE',  ( 0.6343890248118320141, 0.7730139489027949562, 0.000000000000000000 ) ) ;
#25249=ORIENTED_EDGE ( 'NONE', *, *, #908, .T. ) ;
#25321=LINE ( 'NONE', #15405, #4402 ) ;
#25341=CARTESIAN_POINT ( 'NONE',  ( 0.000000000000000000, 0.000000000000000000, 227.6412452697800006 ) ) ;
#25377=STYLED_ITEM ( 'NONE', ( #28820 ), #17428 ) ;
#25400=ORIENTED_EDGE ( 'NONE', *, *, #12156, .F. ) ;
#25412=ORIENTED_EDGE ( 'NONE', *, *, #18275, .F. ) ;
#25445=VERTEX_POINT ( 'NONE', #14743 ) ;
#25458=LINE ( 'NONE', #9074, #13664 ) ;
#25501=VERTEX_POINT ( 'NONE', #30728 ) ;
#25502=STYLED_ITEM ( 'NONE', ( #3478 ), #10658 ) ;
#25540=EDGE_LOOP ( 'NONE', ( #21448, #26932, #23638, #18384 ) ) ;
#25557=CYLINDRICAL_SURFACE ( 'NONE', #13975, 2.100000000000000977 ) ;
#25633=CLOSED_SHELL ( 'NONE', ( #9372, #21588, #25030, #29167, #12526, #8495, #4150, #14698, #23309, #9196, #6543, #24763, #2132, #17933, #19844, #12830, #7578, #9326, #24074, #5236, #28721, #21159, #9245, #28469 ) ) ;
#25664=CARTESIAN_POINT ( 'NONE',  ( 0.000000000000000000, -1.776356839399999804E-15, 227.6412452697800006 ) ) ;
#25681=EDGE_CURVE ( 'NONE', #11841, #125, #13063, .T. ) ;
#25716=ORIENTED_EDGE ( 'NONE', *, *, #19018, .T. ) ;
#25802=CIRCLE ( 'NONE', #13216, 18.00000000000000000 ) ;
#25859=EDGE_CURVE ( 'NONE', #16515, #18650, #7712, .T. ) ;
#25913=CARTESIAN_POINT ( 'NONE',  ( -3.326860148959999819, -4.874695247160000022, 226.6412452697800006 ) ) ;
#25978=ORIENTED_EDGE ( 'NONE', *, *, #1001, .F. ) ;
#26011=ORIENTED_EDGE ( 'NONE', *, *, #3929, .T. ) ;
#26022=DIRECTION ( 'NONE',  ( 0.000000000000000000, 0.000000000000000000, 1.000000000000000000 ) ) ;
#26028=EDGE_CURVE ( 'NONE', #10036, #25445, #27818, .T. ) ;
#26061=VECTOR ( 'NONE', #16144, 1000.000000000000000 ) ;
#26095=ORIENTED_EDGE ( 'NONE', *, *, #26028, .F. ) ;
#26127=CARTESIAN_POINT ( 'NONE',  ( 0.000000000000000000, -1.776356839399999804E-15, 227.6412452697800006 ) ) ;
#26186=EDGE_CURVE ( 'NONE', #553, #1959, #20859, .T. ) ;
#26219=DIRECTION ( 'NONE',  ( 0.6343890248118320141, 0.7730139489027949562, 0.000000000000000000 ) ) ;
#26252=CARTESIAN_POINT ( 'NONE',  ( 1.484924240490000047, 1.484924240490000047, 227.6412452697800006 ) ) ;
#26266=CARTESIAN_POINT ( 'NONE',  ( -12.09628639100000136, -1.465387503939999947, 230.6412452697800006 ) ) ;
#26268=CARTESIAN_POINT ( 'NONE',  ( -4.884981308350000102E-15, -2.100000000000000089, 227.6412452697800006 ) ) ;
#26315=AXIS2_PLACEMENT_3D ( 'NONE', #12738, #26753, #648 ) ;
#26345=CARTESIAN_POINT ( 'NONE',  ( 1.776356839399999804E-15, -5.329070518200000398E-15, 228.3912452697800006 ) ) ;
#26452=DIRECTION ( 'NONE',  ( -0.6343890248118320141, -0.7730139489027949562, 0.000000000000000000 ) ) ;
#26467=DIRECTION ( 'NONE',  ( 0.000000000000000000, 0.000000000000000000, 1.000000000000000000 ) ) ;
#26474=ORIENTED_EDGE ( 'NONE', *, *, #1230, .T. ) ;
#26492=CIRCLE ( 'NONE', #16938, 2.100000000000000089 ) ;
#26534=CARTESIAN_POINT ( 'NONE',  ( 7.636659491170000535, 9.305401069080000198, 229.6412452697800006 ) ) ;
#26559=CARTESIAN_POINT ( 'NONE',  ( 2.033405199262924956, 0.5436710260910023740, 226.6412452697799438 ) ) ;
#26574=CARTESIAN_POINT ( 'NONE',  ( -3.389121577140000063, -11.55088360979999962, 230.6412452697800006 ) ) ;
#26580=DIRECTION ( 'NONE',  ( 1.000000000000000000, 0.000000000000000000, 0.000000000000000000 ) ) ;
#26627=ORIENTED_EDGE ( 'NONE', *, *, #10470, .F. ) ;
#26721=CARTESIAN_POINT ( 'NONE',  ( -4.792542393989999816, 11.13937006400000129, 230.6412452697800006 ) ) ;
#26753=DIRECTION ( 'NONE',  ( 0.000000000000000000, 0.000000000000000000, 1.000000000000000000 ) ) ;
#26756=VERTEX_POINT ( 'NONE', #6686 ) ;
#26815=TOROIDAL_SURFACE ( 'NONE', #21297, 12.03781779390000040, 6.000000000000000000 ) ;
#26845=CARTESIAN_POINT ( 'NONE',  ( 0.000000000000000000, 0.000000000000000000, 229.6412452697800006 ) ) ;
#26864=ORIENTED_EDGE ( 'NONE', *, *, #10530, .F. ) ;
#26932=ORIENTED_EDGE ( 'NONE', *, *, #11187, .F. ) ;
#27048=EDGE_LOOP ( 'NONE', ( #26095, #30980, #2427, #12567, #11690 ) ) ;
#27157=FACE_OUTER_BOUND ( 'NONE', #27048, .T. ) ;
#27169=ORIENTED_EDGE ( 'NONE', *, *, #12468, .F. ) ;
#27187=DIRECTION ( 'NONE',  ( 0.000000000000000000, 0.000000000000000000, 1.000000000000000000 ) ) ;
#27303=CARTESIAN_POINT ( 'NONE',  ( 4.216378357570000000E-10, -6.866525126269999101E-10, 227.6412452697800006 ) ) ;
#27368=B_SPLINE_CURVE_WITH_KNOTS ( 'NONE', 3,
 ( #7874, #3313, #29131, #22067, #29283, #10103, #17331, #19861 ),
 .UNSPECIFIED., .F., .F.,
 ( 4, 2, 2, 4 ),
 ( 0.000000000000000000, 0.2500000000000001110, 0.5000000000000002220, 1.000000000000000000 ),
 .UNSPECIFIED. ) ;
#27408=CARTESIAN_POINT ( 'NONE',  ( 2.100000000000000089, -1.998401444330000344E-15, 226.6412452697800006 ) ) ;
#27424=SHAPE_REPRESENTATION ( 'Plunger Disc', ( #17722 ), #14824 ) ;
#27567=DIRECTION ( 'NONE',  ( 1.000000000000000000, 0.000000000000000000, 0.000000000000000000 ) ) ;
#27649=CARTESIAN_POINT ( 'NONE',  ( 2.220446049249999755E-16, 2.100000000000000089, 226.6412452697800006 ) ) ;
#27652=CARTESIAN_POINT ( 'NONE',  ( -1.583312407113587339, 1.386473476258559545, 226.6412452697800006 ) ) ;
#27677=CARTESIAN_POINT ( 'NONE',  ( 1.094484693600000114, -5.799375430310000468, 226.6412452697800006 ) ) ;
#27765=DIRECTION ( 'NONE',  ( 0.7071067811865475727, 0.7071067811865475727, 0.000000000000000000 ) ) ;
#27793=DIRECTION ( 'NONE',  ( 1.000000000000000000, 0.000000000000000000, 0.000000000000000000 ) ) ;
#27808=FACE_OUTER_BOUND ( 'NONE', #22521, .T. ) ;
#27818=CIRCLE ( 'NONE', #1193, 1.999999999999999112 ) ;
#27824=ORIENTED_EDGE ( 'NONE', *, *, #10530, .T. ) ;
#27837=CARTESIAN_POINT ( 'NONE',  ( 2.862882362280000148, -5.240471012860000499, 226.6412452697800006 ) ) ;
#27840=TOROIDAL_SURFACE ( 'NONE', #11276, 5.792819795519999815, 2.000000000000000000 ) ;
#27865=AXIS2_PLACEMENT_3D ( 'NONE', #25341, #15273, #3782 ) ;
#27911=CARTESIAN_POINT ( 'NONE',  ( 0.000000000000000000, -1.776356839399999804E-15, 227.6412452697800006 ) ) ;
#28121=CARTESIAN_POINT ( 'NONE',  ( 12.09065967409999942, -0.9322763432880000201, 230.6412452697800006 ) ) ;
#28122=B_SPLINE_CURVE_WITH_KNOTS ( 'NONE', 3,
 ( #27649, #10832, #24680, #22631, #20576, #15084, #19956, #15385 ),
 .UNSPECIFIED., .F., .F.,
 ( 4, 2, 2, 4 ),
 ( 0.000000000000000000, 0.2500000000000000000, 0.5000000000000000000, 1.000000000000000000 ),
 .UNSPECIFIED. ) ;
#28272=CARTESIAN_POINT ( 'NONE',  ( 10.21223621230000056, 6.545646588569999480, 230.6412452697800006 ) ) ;
#28284=ORIENTED_EDGE ( 'NONE', *, *, #25859, .T. ) ;
#28317=VERTEX_POINT ( 'NONE', #30413 ) ;
#28415=CARTESIAN_POINT ( 'NONE',  ( -2.070461221339999991, -7.056594471000000368, 228.3912452697800006 ) ) ;
#28418=CARTESIAN_POINT ( 'NONE',  ( -5.729936103060000008, 1.681209052119999825, 226.6412452697800006 ) ) ;
#28421=DIRECTION ( 'NONE',  ( 0.000000000000000000, 0.000000000000000000, 1.000000000000000000 ) ) ;
#28432=CARTESIAN_POINT ( 'NONE',  ( 11.34419785409999903, -4.447397018089999321, 230.6412452697800006 ) ) ;
#28469=ADVANCED_FACE ( 'NONE', ( #25173 ), #687, .F. ) ;
#28524=EDGE_LOOP ( 'NONE', ( #6226, #916, #16060, #19138 ) ) ;
#28559=AXIS2_PLACEMENT_3D ( 'NONE', #14874, #24467, #2901 ) ;
#28572=AXIS2_PLACEMENT_3D ( 'NONE', #2386, #11972, #26452 ) ;
#28610=ORIENTED_EDGE ( 'NONE', *, *, #25681, .F. ) ;
#28630=EDGE_CURVE ( 'NONE', #10257, #25445, #2262, .T. ) ;
#28721=ADVANCED_FACE ( 'NONE', ( #28849 ), #5175, .T. ) ;
#28820=PRESENTATION_STYLE_ASSIGNMENT (( #30895 ) ) ;
#28849=FACE_OUTER_BOUND ( 'NONE', #3048, .T. ) ;
#28893=CARTESIAN_POINT ( 'NONE',  ( 3.326860148959999819, 4.874695247160000022, 226.6412452697800006 ) ) ;
#28911=B_SPLINE_CURVE_WITH_KNOTS ( 'NONE', 5,
 ( #10261, #19864, #18960, #21172, #14096, #14677, #29134, #16595, #23699 ),
 .UNSPECIFIED., .F., .F.,
 ( 6, 3, 6 ),
 ( 46.94504270979999916, 50.80649256949999426, 53.82812367380000040 ),
 .UNSPECIFIED. ) ;
#28924=FACE_OUTER_BOUND ( 'NONE', #13854, .T. ) ;
#28931=CARTESIAN_POINT ( 'NONE',  ( -5.871915332739999549, 10.61013173299999934, 230.6412452697800006 ) ) ;
#28941=ORIENTED_EDGE ( 'NONE', *, *, #458, .F. ) ;
#28966=DIRECTION ( 'NONE',  ( -0.6343890248118320141, -0.7730139489027949562, 0.000000000000000000 ) ) ;
#28975=DIRECTION ( 'NONE',  ( 0.2815395311429195746, 0.9595496299847261490, 0.000000000000000000 ) ) ;
#29004=CARTESIAN_POINT ( 'NONE',  ( -1.484924240490000047, 1.484924240490000047, 227.6412452697800006 ) ) ;
#29065=CARTESIAN_POINT ( 'NONE',  ( -18.00000000000000000, 2.204291436879999808E-15, 230.6412452697800006 ) ) ;
#29089=FACE_BOUND ( 'NONE', #9726, .T. ) ;
#29129=CIRCLE ( 'NONE', #23627, 4.999999999999998224 ) ;
#29131=CARTESIAN_POINT ( 'NONE',  ( 1.280497938707983563, 1.670464374140186781, 226.6412452697800006 ) ) ;
#29134=CARTESIAN_POINT ( 'NONE',  ( 4.198625184269999977, 11.29386254379999954, 230.6412452697800006 ) ) ;
#29143=CARTESIAN_POINT ( 'NONE',  ( -1.630907769230000026, -5.558498091359999727, 229.6412452697800006 ) ) ;
#29167=ADVANCED_FACE ( 'NONE', ( #21742 ), #26815, .T. ) ;
#29174=CARTESIAN_POINT ( 'NONE',  ( 1.630907769230000026, 5.558498091359999727, 227.6412452697800006 ) ) ;
#29203=DIRECTION ( 'NONE',  ( 1.000000000000000000, 0.000000000000000000, 0.000000000000000000 ) ) ;
#29206=ORIENTED_EDGE ( 'NONE', *, *, #23034, .F. ) ;
#29231=CARTESIAN_POINT ( 'NONE',  ( -10.20188979230000115, 6.555481593160000564, 230.6412452697800006 ) ) ;
#29283=CARTESIAN_POINT ( 'NONE',  ( 0.9307262455818937630, 1.887507898842907927, 226.6412452697800290 ) ) ;
#29294=CARTESIAN_POINT ( 'NONE',  ( 0.000000000000000000, 0.000000000000000000, 227.6412452697800006 ) ) ;
#29320=VECTOR ( 'NONE', #15124, 1000.000000000000000 ) ;
#29482=DIRECTION ( 'NONE',  ( 1.000000000000000000, 0.000000000000000000, 0.000000000000000000 ) ) ;
#29579=CARTESIAN_POINT ( 'NONE',  ( 1.484924240490000047, -1.484924240490000047, 226.6412452697800006 ) ) ;
#29603=EDGE_LOOP ( 'NONE', ( #28941, #22193, #5142, #7959 ) ) ;
#29651=DIRECTION ( 'NONE',  ( 0.000000000000000000, 0.000000000000000000, 1.000000000000000000 ) ) ;
#29676=EDGE_CURVE ( 'NONE', #17407, #553, #28122, .T. ) ;
#29797=AXIS2_PLACEMENT_3D ( 'NONE', #10155, #262, #7780 ) ;
#29844=ORIENTED_EDGE ( 'NONE', *, *, #23592, .T. ) ;
#29858=VECTOR ( 'NONE', #21636, 1000.000000000000000 ) ;
#30003=AXIS2_PLACEMENT_3D ( 'NONE', #13955, #4041, #27793 ) ;
#30043=CARTESIAN_POINT ( 'NONE',  ( -1.630907768819999992, -5.558498092260000689, 226.6412452697800006 ) ) ;
#30077=SURFACE_SIDE_STYLE ('',( #8190 ) ) ;
#30118=DIRECTION ( 'NONE',  ( -0.2815395311429195746, -0.9595496299847261490, 0.000000000000000000 ) ) ;
#30182=ORIENTED_EDGE ( 'NONE', *, *, #17902, .T. ) ;
#30201=CARTESIAN_POINT ( 'NONE',  ( 4.054393030549999999, 4.288653550920000335, 226.6412452697800006 ) ) ;
#30258=EDGE_LOOP ( 'NONE', ( #778, #14680, #25412, #16440 ) ) ;
#30342=AXIS2_PLACEMENT_3D ( 'NONE', #26127, #4257, #9 ) ;
#30380=EDGE_CURVE ( 'NONE', #5036, #20819, #22325, .T. ) ;
#30390=AXIS2_PLACEMENT_3D ( 'NONE', #18160, #12834, #27765 ) ;
#30413=CARTESIAN_POINT ( 'NONE',  ( 18.00000000000000000, 0.000000000000000000, 230.6412452697800006 ) ) ;
#30439=CARTESIAN_POINT ( 'NONE',  ( -4.884981308350000102E-15, -2.100000000000000089, 226.6412452697800006 ) ) ;
#30444=DIRECTION ( 'NONE',  ( 0.7730139489027949562, -0.6343890248118320141, 0.000000000000000000 ) ) ;
#30515=CARTESIAN_POINT ( 'NONE',  ( 2.100000000000000089, -1.998401444330000344E-15, 226.6412452697800006 ) ) ;
#30565=CIRCLE ( 'NONE', #16981, 18.00000000000000000 ) ;
#30634=CARTESIAN_POINT ( 'NONE',  ( -5.899424784609999861, -0.1656472027220000087, 226.6412452697800006 ) ) ;
#30648=CARTESIAN_POINT ( 'NONE',  ( 2.525646774360000180, -11.92010449670000050, 230.6412452697800006 ) ) ;
#30726=CARTESIAN_POINT ( 'NONE',  ( -0.2762902765781530823, -2.099999999790001404, 226.6412452697800859 ) ) ;
#30728=CARTESIAN_POINT ( 'NONE',  ( -1.484924240490000047, -1.484924240490000047, 226.6412452697800006 ) ) ;
#30795=CARTESIAN_POINT ( 'NONE',  ( 9.502613819369999604, -7.533418146770000767, 230.6412452697800006 ) ) ;
#30860=EDGE_CURVE ( 'NONE', #20463, #5036, #19320, .T. ) ;
#30895=SURFACE_STYLE_USAGE ( .BOTH. , #2261 ) ;
#30899=DIRECTION ( 'NONE',  ( 0.000000000000000000, 0.000000000000000000, -1.000000000000000000 ) ) ;
#30939=CARTESIAN_POINT ( 'NONE',  ( -2.504034607669999968, -5.302315698040000136, 226.6412452697800006 ) ) ;
#30971=CARTESIAN_POINT ( 'NONE',  ( 1.680165880436631509, 1.289604810889001030, 226.6412452697800006 ) ) ;
#30980=ORIENTED_EDGE ( 'NONE', *, *, #16479, .T. ) ;
#30987=CARTESIAN_POINT ( 'NONE',  ( -11.34419785439999906, 4.447397017599999280, 230.6412452697800006 ) ) ;
#31045=SHAPE_REPRESENTATION_RELATIONSHIP ( 'NONE' , 'NONE' ,  #27424, #17428 ) ;
#31055=AXIS2_PLACEMENT_3D ( 'NONE', #8387, #3520, #25248 ) ;
ENDSEC;
END-ISO-10303-21;
